ISO-10303-21;
HEADER;
/* Generated by software containing ST-Developer
 * from STEP Tools, Inc. (www.steptools.com) 
 */

FILE_DESCRIPTION(
/* description */ ('Independent equipment support assembly with bolted 600 x 500 mm welde
d perimeter frame, four adjustable legs and swivel feet. Nominal overa
ll height 518 mm. No load rating assigned.'),
/* implementation_level */ '2;1');

FILE_NAME(
/* name */ 'Socket head cap screw M6x16.step',
/* time_stamp */ '2026-11-07T17:30:39-08:00',
/* author */ (''),
/* organization */ (''),
/* preprocessor_version */ 'ST-DEVELOPER v20.2',
/* originating_system */ 'Autodesk Translation Framework v15.17.0.0',
/* authorisation */ '');

FILE_SCHEMA (('AUTOMOTIVE_DESIGN { 1 0 10303 214 3 1 1 }'));
ENDSEC;

DATA;
#10=MECHANICAL_DESIGN_GEOMETRIC_PRESENTATION_REPRESENTATION('',(#2222),#63755);
#256=CONICAL_SURFACE('',#15467,2.5,0.785398163397448);
#283=B_SPLINE_SURFACE_WITH_KNOTS('',3,3,((#62572,#62573,#62574,#62575,#62576,
#62577,#62578,#62579,#62580,#62581,#62582,#62583,#62584,#62585,#62586,#62587,
#62588,#62589,#62590,#62591,#62592,#62593,#62594,#62595,#62596,#62597,#62598,
#62599,#62600,#62601,#62602,#62603,#62604,#62605,#62606,#62607,#62608,#62609,
#62610,#62611,#62612,#62613,#62614,#62615,#62616,#62617,#62618,#62619,#62620,
#62621,#62622,#62623,#62624,#62625,#62626,#62627,#62628,#62629,#62630,#62631,
#62632,#62633,#62634,#62635,#62636,#62637,#62638,#62639,#62640,#62641,#62642,
#62643,#62644,#62645,#62646,#62647,#62648,#62649,#62650,#62651,#62652,#62653,
#62654,#62655,#62656,#62657,#62658,#62659,#62660,#62661,#62662,#62663,#62664,
#62665,#62666,#62667,#62668,#62669,#62670,#62671,#62672,#62673),(#62674,
#62675,#62676,#62677,#62678,#62679,#62680,#62681,#62682,#62683,#62684,#62685,
#62686,#62687,#62688,#62689,#62690,#62691,#62692,#62693,#62694,#62695,#62696,
#62697,#62698,#62699,#62700,#62701,#62702,#62703,#62704,#62705,#62706,#62707,
#62708,#62709,#62710,#62711,#62712,#62713,#62714,#62715,#62716,#62717,#62718,
#62719,#62720,#62721,#62722,#62723,#62724,#62725,#62726,#62727,#62728,#62729,
#62730,#62731,#62732,#62733,#62734,#62735,#62736,#62737,#62738,#62739,#62740,
#62741,#62742,#62743,#62744,#62745,#62746,#62747,#62748,#62749,#62750,#62751,
#62752,#62753,#62754,#62755,#62756,#62757,#62758,#62759,#62760,#62761,#62762,
#62763,#62764,#62765,#62766,#62767,#62768,#62769,#62770,#62771,#62772,#62773,
#62774,#62775),(#62776,#62777,#62778,#62779,#62780,#62781,#62782,#62783,
#62784,#62785,#62786,#62787,#62788,#62789,#62790,#62791,#62792,#62793,#62794,
#62795,#62796,#62797,#62798,#62799,#62800,#62801,#62802,#62803,#62804,#62805,
#62806,#62807,#62808,#62809,#62810,#62811,#62812,#62813,#62814,#62815,#62816,
#62817,#62818,#62819,#62820,#62821,#62822,#62823,#62824,#62825,#62826,#62827,
#62828,#62829,#62830,#62831,#62832,#62833,#62834,#62835,#62836,#62837,#62838,
#62839,#62840,#62841,#62842,#62843,#62844,#62845,#62846,#62847,#62848,#62849,
#62850,#62851,#62852,#62853,#62854,#62855,#62856,#62857,#62858,#62859,#62860,
#62861,#62862,#62863,#62864,#62865,#62866,#62867,#62868,#62869,#62870,#62871,
#62872,#62873,#62874,#62875,#62876,#62877),(#62878,#62879,#62880,#62881,
#62882,#62883,#62884,#62885,#62886,#62887,#62888,#62889,#62890,#62891,#62892,
#62893,#62894,#62895,#62896,#62897,#62898,#62899,#62900,#62901,#62902,#62903,
#62904,#62905,#62906,#62907,#62908,#62909,#62910,#62911,#62912,#62913,#62914,
#62915,#62916,#62917,#62918,#62919,#62920,#62921,#62922,#62923,#62924,#62925,
#62926,#62927,#62928,#62929,#62930,#62931,#62932,#62933,#62934,#62935,#62936,
#62937,#62938,#62939,#62940,#62941,#62942,#62943,#62944,#62945,#62946,#62947,
#62948,#62949,#62950,#62951,#62952,#62953,#62954,#62955,#62956,#62957,#62958,
#62959,#62960,#62961,#62962,#62963,#62964,#62965,#62966,#62967,#62968,#62969,
#62970,#62971,#62972,#62973,#62974,#62975,#62976,#62977,#62978,#62979)),
 .UNSPECIFIED.,.F.,.F.,.F.,(4,4),(4,1,1,1,1,1,1,1,1,1,1,1,1,1,1,1,1,1,1,
1,1,1,1,1,1,1,1,1,1,1,1,1,1,1,1,1,1,1,1,1,1,1,1,1,1,1,1,1,1,1,1,1,1,1,1,
1,1,1,1,1,1,1,1,1,1,1,1,1,1,1,1,1,1,1,1,1,1,1,1,1,1,1,1,1,1,1,1,1,1,1,1,
1,1,1,1,1,1,1,1,4),(0.,0.0658467982010768),(11.6150328478182,12.6069034617266,
13.598774075635,14.5906446895433,15.5825153034517,16.5743859173601,17.5662565312685,
18.5581271451769,19.5499977590852,20.5418683729936,21.533738986902,22.5256096008104,
23.5174802147187,24.5093508286271,25.5012214425355,26.4930920564439,27.4849626703523,
28.4768332842606,29.468703898169,30.4605745120774,31.4524451259858,32.4443157398941,
33.4361863538025,34.4280569677109,35.4199275816193,36.4117981955277,37.403668809436,
38.3955394233444,39.3874100372528,40.3792806511612,41.3711512650695,42.3630218789779,
43.3548924928863,44.3467631067947,45.3386337207031,46.3305043346114,47.3223749485198,
48.3142455624282,49.3061161763366,50.2979867902449,51.2898574041533,52.2817280180617,
53.2735986319701,54.2654692458785,55.2573398597868,56.2492104736952,57.2410810876036,
58.232951701512,59.2248223154203,60.2166929293287,61.2085635432371,62.2004341571455,
63.1923047710539,64.1841753849622,65.1760459988706,66.167916612779,67.1597872266874,
68.1516578405957,69.1435284545041,70.1353990684125,71.1272696823209,72.1191402962293,
73.1110109101376,74.102881524046,75.0947521379544,76.0866227518628,77.0784933657711,
78.0703639796795,79.0622345935879,80.0541052074963,81.0459758214047,82.037846435313,
83.0297170492214,84.0215876631298,85.0134582770382,86.0053288909465,86.9971995048549,
87.9890701187633,88.9809407326717,89.9728113465801,90.9646819604884,91.9565525743968,
92.9484231883052,93.9402938022136,94.9321644161219,95.9240350300303,96.9159056439387,
97.9077762578471,98.8996468717555,99.8915174856638,100.883388099572,101.875258713481,
102.867129327389,103.858999941297,104.850870555206,105.842741169114,106.834611783022,
107.826482396931,108.818353010839,109.810223624748),.UNSPECIFIED.);
#284=B_SPLINE_SURFACE_WITH_KNOTS('',3,3,((#63108,#63109,#63110,#63111,#63112,
#63113,#63114,#63115,#63116,#63117,#63118,#63119,#63120,#63121,#63122,#63123,
#63124,#63125,#63126,#63127,#63128,#63129,#63130,#63131,#63132,#63133,#63134,
#63135,#63136,#63137,#63138,#63139,#63140,#63141,#63142,#63143,#63144,#63145,
#63146,#63147,#63148,#63149,#63150,#63151,#63152,#63153,#63154,#63155,#63156,
#63157,#63158,#63159,#63160,#63161,#63162,#63163,#63164,#63165,#63166,#63167,
#63168,#63169,#63170,#63171,#63172,#63173,#63174,#63175,#63176,#63177,#63178,
#63179,#63180,#63181,#63182,#63183,#63184,#63185,#63186,#63187,#63188,#63189,
#63190,#63191,#63192,#63193,#63194,#63195,#63196,#63197,#63198,#63199,#63200,
#63201,#63202,#63203,#63204,#63205,#63206,#63207,#63208,#63209,#63210,#63211),
(#63212,#63213,#63214,#63215,#63216,#63217,#63218,#63219,#63220,#63221,
#63222,#63223,#63224,#63225,#63226,#63227,#63228,#63229,#63230,#63231,#63232,
#63233,#63234,#63235,#63236,#63237,#63238,#63239,#63240,#63241,#63242,#63243,
#63244,#63245,#63246,#63247,#63248,#63249,#63250,#63251,#63252,#63253,#63254,
#63255,#63256,#63257,#63258,#63259,#63260,#63261,#63262,#63263,#63264,#63265,
#63266,#63267,#63268,#63269,#63270,#63271,#63272,#63273,#63274,#63275,#63276,
#63277,#63278,#63279,#63280,#63281,#63282,#63283,#63284,#63285,#63286,#63287,
#63288,#63289,#63290,#63291,#63292,#63293,#63294,#63295,#63296,#63297,#63298,
#63299,#63300,#63301,#63302,#63303,#63304,#63305,#63306,#63307,#63308,#63309,
#63310,#63311,#63312,#63313,#63314,#63315),(#63316,#63317,#63318,#63319,
#63320,#63321,#63322,#63323,#63324,#63325,#63326,#63327,#63328,#63329,#63330,
#63331,#63332,#63333,#63334,#63335,#63336,#63337,#63338,#63339,#63340,#63341,
#63342,#63343,#63344,#63345,#63346,#63347,#63348,#63349,#63350,#63351,#63352,
#63353,#63354,#63355,#63356,#63357,#63358,#63359,#63360,#63361,#63362,#63363,
#63364,#63365,#63366,#63367,#63368,#63369,#63370,#63371,#63372,#63373,#63374,
#63375,#63376,#63377,#63378,#63379,#63380,#63381,#63382,#63383,#63384,#63385,
#63386,#63387,#63388,#63389,#63390,#63391,#63392,#63393,#63394,#63395,#63396,
#63397,#63398,#63399,#63400,#63401,#63402,#63403,#63404,#63405,#63406,#63407,
#63408,#63409,#63410,#63411,#63412,#63413,#63414,#63415,#63416,#63417,#63418,
#63419),(#63420,#63421,#63422,#63423,#63424,#63425,#63426,#63427,#63428,
#63429,#63430,#63431,#63432,#63433,#63434,#63435,#63436,#63437,#63438,#63439,
#63440,#63441,#63442,#63443,#63444,#63445,#63446,#63447,#63448,#63449,#63450,
#63451,#63452,#63453,#63454,#63455,#63456,#63457,#63458,#63459,#63460,#63461,
#63462,#63463,#63464,#63465,#63466,#63467,#63468,#63469,#63470,#63471,#63472,
#63473,#63474,#63475,#63476,#63477,#63478,#63479,#63480,#63481,#63482,#63483,
#63484,#63485,#63486,#63487,#63488,#63489,#63490,#63491,#63492,#63493,#63494,
#63495,#63496,#63497,#63498,#63499,#63500,#63501,#63502,#63503,#63504,#63505,
#63506,#63507,#63508,#63509,#63510,#63511,#63512,#63513,#63514,#63515,#63516,
#63517,#63518,#63519,#63520,#63521,#63522,#63523)),.UNSPECIFIED.,.F.,.F.,
 .F.,(4,4),(4,1,1,1,1,1,1,1,1,1,1,1,1,1,1,1,1,1,1,1,1,1,1,1,1,1,1,1,1,1,
1,1,1,1,1,1,1,1,1,1,1,1,1,1,1,1,1,1,1,1,1,1,1,1,1,1,1,1,1,1,1,1,1,1,1,1,
1,1,1,1,1,1,1,1,1,1,1,1,1,1,1,1,1,1,1,1,1,1,1,1,1,1,1,1,1,1,1,1,1,1,1,4),
(0.,0.0658467982010768),(8.30747755240101,9.30018873014199,10.292899907883,
11.2856110856239,12.2783222633649,13.2710334411059,14.2637446188469,15.2564557965878,
16.2491669743288,17.2418781520698,18.2345893298108,19.2273005075518,20.2200116852927,
21.2127228630337,22.2054340407747,23.1981452185157,24.1908563962566,25.1835675739976,
26.1762787517386,27.1689899294796,28.1617011072206,29.1544122849615,30.1471234627025,
31.1398346404435,32.1325458181845,33.1252569959254,34.1179681736664,35.1106793514074,
36.1033905291484,37.0961017068893,38.0888128846303,39.0815240623713,40.0742352401123,
41.0669464178533,42.0596575955942,43.0523687733352,44.0450799510762,45.0377911288172,
46.0305023065581,47.0232134842991,48.0159246620401,49.0086358397811,50.001347017522,
50.994058195263,51.986769373004,52.979480550745,53.972191728486,54.9649029062269,
55.9576140839679,56.9503252617089,57.9430364394499,58.9357476171908,59.9284587949318,
60.9211699726728,61.9138811504138,62.9065923281547,63.8993035058957,64.8920146836367,
65.8847258613777,66.8774370391187,67.8701482168596,68.8628593946006,69.8555705723416,
70.8482817500825,71.8409929278235,72.8337041055645,73.8264152833055,74.8191264610465,
75.8118376387874,76.8045488165284,77.7972599942694,78.7899711720104,79.7826823497514,
80.7753935274923,81.7681047052333,82.7608158829743,83.7535270607153,84.7462382384562,
85.7389494161972,86.7316605939382,87.7243717716792,88.7170829494201,89.7097941271611,
90.7025053049021,91.6952164826431,92.687927660384,93.680638838125,94.673350015866,
95.666061193607,96.658772371348,97.6514835490889,98.6441947268299,99.6369059045709,
100.629617082312,101.622328260053,102.615039437794,103.607750615535,104.600461793276,
105.593172971017,106.585884148758,107.578595326499,108.57130650424),
 .UNSPECIFIED.);
#476=CIRCLE('',#15436,2.942);
#477=CIRCLE('',#15452,2.37175);
#478=CIRCLE('',#15468,2.942);
#479=CIRCLE('',#15469,2.);
#480=CIRCLE('',#15471,2.37175);
#481=CIRCLE('',#15481,5.);
#482=CIRCLE('',#15483,5.);
#1521=B_SPLINE_CURVE_WITH_KNOTS('',3,(#61164,#61165,#61166,#61167,#61168,
#61169,#61170,#61171,#61172,#61173),.UNSPECIFIED.,.F.,.F.,(4,3,3,4),(-4.09293042013066,
-3.96748245563351,-2.97561184172513,-2.06863817490915),.UNSPECIFIED.);
#1522=B_SPLINE_CURVE_WITH_KNOTS('',3,(#61176,#61177,#61178,#61179,#61180,
#61181,#61182),.UNSPECIFIED.,.F.,.F.,(4,3,4),(0.,0.992711177740983,1.1173004083682),
 .UNSPECIFIED.);
#1523=B_SPLINE_CURVE_WITH_KNOTS('',3,(#61187,#61188,#61189,#61190,#61191,
#61192,#61193,#61194,#61195,#61196,#61197,#61198,#61199,#61200,#61201,#61202,
#61203,#61204,#61205,#61206,#61207,#61208),.UNSPECIFIED.,.F.,.F.,(4,3,3,
3,3,3,3,4),(-10.3761157273102,-9.91870613908378,-8.9268355251754,-7.93496491126702,
-6.94309429735864,-5.95122368345026,-4.95935306954189,-4.09293042013066),
 .UNSPECIFIED.);
#1524=B_SPLINE_CURVE_WITH_KNOTS('',3,(#61209,#61210,#61211,#61212,#61213,
#61214,#61215,#61216,#61217,#61218,#61219,#61220,#61221,#61222,#61223,#61224,
#61225,#61226,#61227,#61228,#61229,#61230),.UNSPECIFIED.,.F.,.F.,(4,3,3,
3,3,3,3,4),(1.1173004083682,1.98542235548196,2.97813353322293,3.97084471096391,
4.96355588870488,5.95626706644586,6.94897824418683,7.40048571554779),
 .UNSPECIFIED.);
#1525=B_SPLINE_CURVE_WITH_KNOTS('',3,(#61235,#61236,#61237,#61238,#61239,
#61240,#61241,#61242,#61243,#61244,#61245,#61246,#61247,#61248,#61249,#61250,
#61251,#61252,#61253,#61254,#61255,#61256),.UNSPECIFIED.,.F.,.F.,(4,3,3,
3,3,3,3,4),(-16.6593010344898,-15.869929822534,-14.8780592086257,-13.8861885947173,
-12.8943179808089,-11.9024473669005,-10.9105767529922,-10.3761157273102),
 .UNSPECIFIED.);
#1526=B_SPLINE_CURVE_WITH_KNOTS('',3,(#61257,#61258,#61259,#61260,#61261,
#61262,#61263,#61264,#61265,#61266,#61267,#61268,#61269,#61270,#61271,#61272,
#61273,#61274,#61275,#61276,#61277,#61278),.UNSPECIFIED.,.F.,.F.,(4,3,3,
3,3,3,3,4),(7.40048571554779,7.94168942192781,8.93440059966879,9.92711177740977,
10.9198229551507,11.9125341328917,12.9052453106327,13.6836710227274),
 .UNSPECIFIED.);
#1527=B_SPLINE_CURVE_WITH_KNOTS('',3,(#61283,#61284,#61285,#61286,#61287,
#61288,#61289,#61290,#61291,#61292,#61293,#61294,#61295,#61296,#61297,#61298,
#61299,#61300,#61301,#61302,#61303,#61304,#61305,#61306,#61307),
 .UNSPECIFIED.,.F.,.F.,(4,3,3,3,3,3,3,3,4),(-22.9424863416694,-22.8130241198927,
-21.8211535059843,-20.8292828920759,-19.8374122781676,-18.8455416642592,
-17.8536710503508,-16.8618004364424,-16.6593010344898),.UNSPECIFIED.);
#1528=B_SPLINE_CURVE_WITH_KNOTS('',3,(#61308,#61309,#61310,#61311,#61312,
#61313,#61314,#61315,#61316,#61317,#61318,#61319,#61320,#61321,#61322,#61323,
#61324,#61325,#61326,#61327,#61328,#61329,#61330,#61331,#61332),
 .UNSPECIFIED.,.F.,.F.,(4,3,3,3,3,3,3,3,4),(13.6836710227274,13.8979564883737,
14.8906676661147,15.8833788438556,16.8760900215966,17.8688011993376,18.8615123770786,
19.8542235548195,19.966856329907),.UNSPECIFIED.);
#1529=B_SPLINE_CURVE_WITH_KNOTS('',3,(#61337,#61338,#61339,#61340,#61341,
#61342,#61343,#61344,#61345,#61346,#61347,#61348,#61349,#61350,#61351,#61352,
#61353,#61354,#61355,#61356,#61357,#61358),.UNSPECIFIED.,.F.,.F.,(4,3,3,
3,3,3,3,4),(-29.225671648849,-28.764247803343,-27.7723771894346,-26.7805065755262,
-25.7886359616178,-24.7967653477094,-23.8048947338011,-22.9424863416694),
 .UNSPECIFIED.);
#1530=B_SPLINE_CURVE_WITH_KNOTS('',3,(#61359,#61360,#61361,#61362,#61363,
#61364,#61365,#61366,#61367,#61368,#61369,#61370,#61371,#61372,#61373,#61374,
#61375,#61376,#61377,#61378,#61379,#61380),.UNSPECIFIED.,.F.,.F.,(4,3,3,
3,3,3,3,4),(19.966856329907,20.8469347325605,21.8396459103015,22.8323570880425,
23.8250682657834,24.8177794435244,25.8104906212654,26.2500416370865),
 .UNSPECIFIED.);
#1531=B_SPLINE_CURVE_WITH_KNOTS('',3,(#61385,#61386,#61387,#61388,#61389,
#61390,#61391,#61392,#61393,#61394,#61395,#61396,#61397,#61398,#61399,#61400,
#61401,#61402,#61403,#61404,#61405,#61406),.UNSPECIFIED.,.F.,.F.,(4,3,3,
3,3,3,3,4),(-35.5088569560286,-34.7154714867932,-33.7236008728848,-32.7317302589765,
-31.7398596450681,-30.7479890311597,-29.7561184172513,-29.225671648849),
 .UNSPECIFIED.);
#1532=B_SPLINE_CURVE_WITH_KNOTS('',3,(#61407,#61408,#61409,#61410,#61411,
#61412,#61413,#61414,#61415,#61416,#61417,#61418,#61419,#61420,#61421,#61422,
#61423,#61424,#61425,#61426,#61427,#61428),.UNSPECIFIED.,.F.,.F.,(4,3,3,
3,3,3,3,4),(26.2500416370865,26.8032017990064,27.7959129767474,28.7886241544883,
29.7813353322293,30.7740465099703,31.7667576877113,32.5332269442661),
 .UNSPECIFIED.);
#1533=B_SPLINE_CURVE_WITH_KNOTS('',3,(#61433,#61434,#61435,#61436,#61437,
#61438,#61439,#61440,#61441,#61442,#61443,#61444,#61445,#61446,#61447,#61448,
#61449,#61450,#61451,#61452,#61453,#61454,#61455,#61456,#61457),
 .UNSPECIFIED.,.F.,.F.,(4,3,3,3,3,3,3,3,4),(-41.7920422632082,-41.6585657841519,
-40.6666951702435,-39.6748245563351,-38.6829539424267,-37.6910833285184,
-36.69921271461,-35.7073421007016,-35.5088569560286),.UNSPECIFIED.);
#1534=B_SPLINE_CURVE_WITH_KNOTS('',3,(#61458,#61459,#61460,#61461,#61462,
#61463,#61464,#61465,#61466,#61467,#61468,#61469,#61470,#61471,#61472,#61473,
#61474,#61475,#61476,#61477,#61478,#61479,#61480,#61481,#61482),
 .UNSPECIFIED.,.F.,.F.,(4,3,3,3,3,3,3,3,4),(32.5332269442661,32.7594688654522,
33.7521800431932,34.7448912209342,35.7376023986752,36.7303135764161,37.7230247541571,
38.7157359318981,38.8164122514457),.UNSPECIFIED.);
#1535=B_SPLINE_CURVE_WITH_KNOTS('',3,(#61487,#61488,#61489,#61490,#61491,
#61492,#61493,#61494,#61495,#61496,#61497,#61498,#61499,#61500,#61501,#61502,
#61503,#61504,#61505,#61506,#61507,#61508),.UNSPECIFIED.,.F.,.F.,(4,3,3,
3,3,3,3,4),(-48.0752275703878,-47.6097894676021,-46.6179188536938,-45.6260482397854,
-44.634177625877,-43.6423070119686,-42.6504363980602,-41.7920422632082),
 .UNSPECIFIED.);
#1536=B_SPLINE_CURVE_WITH_KNOTS('',3,(#61509,#61510,#61511,#61512,#61513,
#61514,#61515,#61516,#61517,#61518,#61519,#61520,#61521,#61522,#61523,#61524,
#61525,#61526,#61527,#61528,#61529,#61530),.UNSPECIFIED.,.F.,.F.,(4,3,3,
3,3,3,3,4),(38.8164122514457,39.7084471096391,40.7011582873801,41.693869465121,
42.686580642862,43.679291820603,44.672002998344,45.0995975586253),
 .UNSPECIFIED.);
#1537=B_SPLINE_CURVE_WITH_KNOTS('',3,(#61535,#61536,#61537,#61538,#61539,
#61540,#61541,#61542,#61543,#61544,#61545,#61546,#61547,#61548,#61549,#61550,
#61551,#61552,#61553,#61554,#61555,#61556),.UNSPECIFIED.,.F.,.F.,(4,3,3,
3,3,3,3,4),(-54.3584128775674,-53.5610131510524,-52.569142537144,-51.5772719232356,
-50.5854013093273,-49.5935306954189,-48.6016600815105,-48.0752275703878),
 .UNSPECIFIED.);
#1538=B_SPLINE_CURVE_WITH_KNOTS('',3,(#61557,#61558,#61559,#61560,#61561,
#61562,#61563,#61564,#61565,#61566,#61567,#61568,#61569,#61570,#61571,#61572,
#61573,#61574,#61575,#61576,#61577,#61578),.UNSPECIFIED.,.F.,.F.,(4,3,3,
3,3,3,3,4),(45.0995975586253,45.6647141760849,46.6574253538259,47.6501365315669,
48.6428477093079,49.6355588870488,50.6282700647898,51.3827828658049),
 .UNSPECIFIED.);
#1539=B_SPLINE_CURVE_WITH_KNOTS('',3,(#61583,#61584,#61585,#61586,#61587,
#61588,#61589,#61590,#61591,#61592,#61593,#61594,#61595,#61596,#61597,#61598,
#61599,#61600,#61601,#61602,#61603,#61604,#61605,#61606,#61607),
 .UNSPECIFIED.,.F.,.F.,(4,3,3,3,3,3,3,3,4),(-60.641598184747,-60.5041074484111,
-59.5122368345027,-58.5203662205943,-57.5284956066859,-56.5366249927775,
-55.5447543788692,-54.5528837649608,-54.3584128775674),.UNSPECIFIED.);
#1540=B_SPLINE_CURVE_WITH_KNOTS('',3,(#61608,#61609,#61610,#61611,#61612,
#61613,#61614,#61615,#61616,#61617,#61618,#61619,#61620,#61621,#61622,#61623,
#61624,#61625,#61626,#61627,#61628,#61629,#61630,#61631,#61632),
 .UNSPECIFIED.,.F.,.F.,(4,3,3,3,3,3,3,3,4),(51.3827828658049,51.6209812425308,
52.6136924202718,53.6064035980127,54.5991147757537,55.5918259534947,56.5845371312357,
57.5772483089767,57.6659681729845),.UNSPECIFIED.);
#1541=B_SPLINE_CURVE_WITH_KNOTS('',3,(#61637,#61638,#61639,#61640,#61641,
#61642,#61643,#61644,#61645,#61646,#61647,#61648,#61649,#61650,#61651,#61652,
#61653,#61654,#61655,#61656,#61657,#61658),.UNSPECIFIED.,.F.,.F.,(4,3,3,
3,3,3,3,4),(-66.9247834919266,-66.4553311318613,-65.4634605179529,-64.4715899040445,
-63.4797192901362,-62.4878486762278,-61.4959780623194,-60.641598184747),
 .UNSPECIFIED.);
#1542=B_SPLINE_CURVE_WITH_KNOTS('',3,(#61659,#61660,#61661,#61662,#61663,
#61664,#61665,#61666,#61667,#61668,#61669,#61670,#61671,#61672,#61673,#61674,
#61675,#61676,#61677,#61678,#61679,#61680),.UNSPECIFIED.,.F.,.F.,(4,3,3,
3,3,3,3,4),(57.6659681729845,58.5699594867177,59.5626706644586,60.5553818421996,
61.5480930199406,62.5408041976816,63.5335153754225,63.9491534801641),
 .UNSPECIFIED.);
#1543=B_SPLINE_CURVE_WITH_KNOTS('',3,(#61685,#61686,#61687,#61688,#61689,
#61690,#61691,#61692,#61693,#61694,#61695,#61696,#61697,#61698,#61699,#61700,
#61701,#61702,#61703,#61704,#61705,#61706),.UNSPECIFIED.,.F.,.F.,(4,3,3,
3,3,3,3,4),(-73.2079687991062,-72.4065548153116,-71.4146842014032,-70.4228135874948,
-69.4309429735864,-68.4390723596781,-67.4472017457697,-66.9247834919266),
 .UNSPECIFIED.);
#1544=B_SPLINE_CURVE_WITH_KNOTS('',3,(#61707,#61708,#61709,#61710,#61711,
#61712,#61713,#61714,#61715,#61716,#61717,#61718,#61719,#61720,#61721,#61722,
#61723,#61724,#61725,#61726,#61727,#61728),.UNSPECIFIED.,.F.,.F.,(4,3,3,
3,3,3,3,4),(63.9491534801641,64.5262265531635,65.5189377309045,66.5116489086455,
67.5043600863864,68.4970712641274,69.4897824418684,70.2323387873437),
 .UNSPECIFIED.);
#1545=B_SPLINE_CURVE_WITH_KNOTS('',3,(#61733,#61734,#61735,#61736,#61737,
#61738,#61739,#61740,#61741,#61742,#61743,#61744,#61745,#61746,#61747,#61748,
#61749,#61750,#61751,#61752,#61753,#61754,#61755,#61756,#61757),
 .UNSPECIFIED.,.F.,.F.,(4,3,3,3,3,3,3,3,4),(-79.4911541062857,-79.3496491126702,
-78.3577784987618,-77.3659078848535,-76.3740372709451,-75.3821666570367,
-74.3902960431283,-73.3984254292199,-73.2079687991062),.UNSPECIFIED.);
#1546=B_SPLINE_CURVE_WITH_KNOTS('',3,(#61758,#61759,#61760,#61761,#61762,
#61763,#61764,#61765,#61766,#61767,#61768,#61769,#61770,#61771,#61772,#61773,
#61774,#61775,#61776,#61777,#61778,#61779,#61780,#61781,#61782),
 .UNSPECIFIED.,.F.,.F.,(4,3,3,3,3,3,3,3,4),(70.2323387873437,70.4824936196094,
71.4752047973503,72.4679159750913,73.4606271528323,74.4533383305733,75.4460495083142,
76.4387606860552,76.5155240945233),.UNSPECIFIED.);
#1547=B_SPLINE_CURVE_WITH_KNOTS('',3,(#61787,#61788,#61789,#61790,#61791,
#61792,#61793,#61794,#61795,#61796,#61797,#61798,#61799,#61800,#61801,#61802,
#61803,#61804,#61805,#61806,#61807,#61808),.UNSPECIFIED.,.F.,.F.,(4,3,3,
3,3,3,3,4),(-85.7743394134653,-85.3008727961205,-84.3090021822121,-83.3171315683037,
-82.3252609543953,-81.333390340487,-80.3415197265786,-79.4911541062857),
 .UNSPECIFIED.);
#1548=B_SPLINE_CURVE_WITH_KNOTS('',3,(#61809,#61810,#61811,#61812,#61813,
#61814,#61815,#61816,#61817,#61818,#61819,#61820,#61821,#61822,#61823,#61824,
#61825,#61826,#61827,#61828,#61829,#61830),.UNSPECIFIED.,.F.,.F.,(4,3,3,
3,3,3,3,4),(76.5155240945233,77.4314718637962,78.4241830415372,79.4168942192782,
80.4096053970191,81.4023165747601,82.3950277525011,82.7987094017029),
 .UNSPECIFIED.);
#1549=B_SPLINE_CURVE_WITH_KNOTS('',3,(#61835,#61836,#61837,#61838,#61839,
#61840,#61841,#61842,#61843,#61844,#61845,#61846,#61847,#61848,#61849,#61850,
#61851,#61852,#61853,#61854,#61855,#61856),.UNSPECIFIED.,.F.,.F.,(4,3,3,
3,3,3,3,4),(-92.0575247206449,-91.2520964795708,-90.2602258656624,-89.268355251754,
-88.2764846378456,-87.2846140239373,-86.2927434100289,-85.7743394134653),
 .UNSPECIFIED.);
#1550=B_SPLINE_CURVE_WITH_KNOTS('',3,(#61857,#61858,#61859,#61860,#61861,
#61862,#61863,#61864,#61865,#61866,#61867,#61868,#61869,#61870,#61871,#61872,
#61873,#61874,#61875,#61876,#61877,#61878),.UNSPECIFIED.,.F.,.F.,(4,3,3,
3,3,3,3,4),(82.7987094017029,83.3877389302421,84.380450107983,85.373161285724,
86.365872463465,87.358583641206,88.351294818947,89.0818947088825),
 .UNSPECIFIED.);
#1551=B_SPLINE_CURVE_WITH_KNOTS('',3,(#61884,#61885,#61886,#61887,#61888,
#61889,#61890,#61891,#61892,#61893),.UNSPECIFIED.,.F.,.F.,(4,1,1,1,1,1,
1,4),(103.672557568463,103.858999941297,104.850870555206,105.842741169114,
106.834611783022,107.826482396931,108.818353010839,109.810223624748),
 .UNSPECIFIED.);
#1552=B_SPLINE_CURVE_WITH_KNOTS('',3,(#61896,#61897,#61898,#61899,#61900,
#61901,#61902,#61903),.UNSPECIFIED.,.F.,.F.,(4,1,1,1,1,4),(103.672557568463,
104.600461793276,105.593172971017,106.585884148758,107.578595326499,108.57130650424),
 .UNSPECIFIED.);
#1553=B_SPLINE_CURVE_WITH_KNOTS('',3,(#61908,#61909,#61910,#61911,#61912,
#61913,#61914,#61915,#61916,#61917),.UNSPECIFIED.,.F.,.F.,(4,1,1,1,1,1,
1,4),(97.3893722612836,97.9077762578471,98.8996468717555,99.8915174856638,
100.883388099572,101.875258713481,102.867129327389,103.672557568463),
 .UNSPECIFIED.);
#1554=B_SPLINE_CURVE_WITH_KNOTS('',3,(#61918,#61919,#61920,#61921,#61922,
#61923,#61924,#61925,#61926,#61927,#61928),.UNSPECIFIED.,.F.,.F.,(4,1,1,
1,1,1,1,1,4),(97.3893722612836,97.6514835490889,98.6441947268299,99.6369059045709,
100.629617082312,101.622328260053,102.615039437794,103.607750615535,103.672557568463),
 .UNSPECIFIED.);
#1555=B_SPLINE_CURVE_WITH_KNOTS('',3,(#61933,#61934,#61935,#61936,#61937,
#61938,#61939,#61940,#61941,#61942),.UNSPECIFIED.,.F.,.F.,(4,1,1,1,1,1,
1,4),(91.106186954104,91.9565525743968,92.9484231883052,93.9402938022136,
94.9321644161219,95.9240350300303,96.9159056439387,97.3893722612836),
 .UNSPECIFIED.);
#1556=B_SPLINE_CURVE_WITH_KNOTS('',3,(#61943,#61944,#61945,#61946,#61947,
#61948,#61949,#61950,#61951,#61952),.UNSPECIFIED.,.F.,.F.,(4,1,1,1,1,1,
1,4),(91.106186954104,91.6952164826431,92.687927660384,93.680638838125,
94.673350015866,95.666061193607,96.658772371348,97.3893722612836),
 .UNSPECIFIED.);
#1557=B_SPLINE_CURVE_WITH_KNOTS('',3,(#61957,#61958,#61959,#61960,#61961,
#61962,#61963,#61964,#61965,#61966,#61967),.UNSPECIFIED.,.F.,.F.,(4,1,1,
1,1,1,1,1,4),(84.8230016469244,85.0134582770382,86.0053288909465,86.9971995048549,
87.9890701187633,88.9809407326717,89.9728113465801,90.9646819604884,91.106186954104),
 .UNSPECIFIED.);
#1558=B_SPLINE_CURVE_WITH_KNOTS('',3,(#61968,#61969,#61970,#61971,#61972,
#61973,#61974,#61975,#61976,#61977),.UNSPECIFIED.,.F.,.F.,(4,1,1,1,1,1,
1,4),(84.8230016469244,85.7389494161972,86.7316605939382,87.7243717716792,
88.7170829494201,89.7097941271611,90.7025053049021,91.106186954104),
 .UNSPECIFIED.);
#1559=B_SPLINE_CURVE_WITH_KNOTS('',3,(#61982,#61983,#61984,#61985,#61986,
#61987,#61988,#61989,#61990,#61991),.UNSPECIFIED.,.F.,.F.,(4,1,1,1,1,1,
1,4),(78.5398163397448,79.0622345935879,80.0541052074963,81.0459758214047,
82.037846435313,83.0297170492214,84.0215876631298,84.8230016469244),
 .UNSPECIFIED.);
#1560=B_SPLINE_CURVE_WITH_KNOTS('',3,(#61992,#61993,#61994,#61995,#61996,
#61997,#61998,#61999,#62000,#62001,#62002),.UNSPECIFIED.,.F.,.F.,(4,1,1,
1,1,1,1,1,4),(78.5398163397448,78.7899711720104,79.7826823497514,80.7753935274923,
81.7681047052333,82.7608158829743,83.7535270607153,84.7462382384562,84.8230016469244),
 .UNSPECIFIED.);
#1561=B_SPLINE_CURVE_WITH_KNOTS('',3,(#62007,#62008,#62009,#62010,#62011,
#62012,#62013,#62014,#62015,#62016),.UNSPECIFIED.,.F.,.F.,(4,1,1,1,1,1,
1,4),(72.2566310325652,73.1110109101376,74.102881524046,75.0947521379544,
76.0866227518628,77.0784933657711,78.0703639796795,78.5398163397448),
 .UNSPECIFIED.);
#1562=B_SPLINE_CURVE_WITH_KNOTS('',3,(#62017,#62018,#62019,#62020,#62021,
#62022,#62023,#62024,#62025,#62026),.UNSPECIFIED.,.F.,.F.,(4,1,1,1,1,1,
1,4),(72.2566310325652,72.8337041055645,73.8264152833055,74.8191264610465,
75.8118376387874,76.8045488165284,77.7972599942694,78.5398163397448),
 .UNSPECIFIED.);
#1563=B_SPLINE_CURVE_WITH_KNOTS('',3,(#62031,#62032,#62033,#62034,#62035,
#62036,#62037,#62038,#62039,#62040,#62041),.UNSPECIFIED.,.F.,.F.,(4,1,1,
1,1,1,1,1,4),(65.9734457253856,66.167916612779,67.1597872266874,68.1516578405957,
69.1435284545041,70.1353990684125,71.1272696823209,72.1191402962293,72.2566310325652),
 .UNSPECIFIED.);
#1564=B_SPLINE_CURVE_WITH_KNOTS('',3,(#62042,#62043,#62044,#62045,#62046,
#62047,#62048,#62049,#62050,#62051),.UNSPECIFIED.,.F.,.F.,(4,1,1,1,1,1,
1,4),(65.9734457253856,66.8774370391187,67.8701482168596,68.8628593946006,
69.8555705723416,70.8482817500825,71.8409929278235,72.2566310325652),
 .UNSPECIFIED.);
#1565=B_SPLINE_CURVE_WITH_KNOTS('',3,(#62056,#62057,#62058,#62059,#62060,
#62061,#62062,#62063,#62064,#62065),.UNSPECIFIED.,.F.,.F.,(4,1,1,1,1,1,
1,4),(59.6902604182061,60.2166929293287,61.2085635432371,62.2004341571455,
63.1923047710539,64.1841753849622,65.1760459988706,65.9734457253856),
 .UNSPECIFIED.);
#1566=B_SPLINE_CURVE_WITH_KNOTS('',3,(#62066,#62067,#62068,#62069,#62070,
#62071,#62072,#62073,#62074,#62075,#62076),.UNSPECIFIED.,.F.,.F.,(4,1,1,
1,1,1,1,1,4),(59.690260418206,59.9284587949318,60.9211699726728,61.9138811504138,
62.9065923281547,63.8993035058957,64.8920146836367,65.8847258613777,65.9734457253856),
 .UNSPECIFIED.);
#1567=B_SPLINE_CURVE_WITH_KNOTS('',3,(#62081,#62082,#62083,#62084,#62085,
#62086,#62087,#62088,#62089,#62090),.UNSPECIFIED.,.F.,.F.,(4,1,1,1,1,1,
1,4),(53.4070751110265,54.2654692458785,55.2573398597868,56.2492104736952,
57.2410810876036,58.232951701512,59.2248223154203,59.6902604182061),
 .UNSPECIFIED.);
#1568=B_SPLINE_CURVE_WITH_KNOTS('',3,(#62091,#62092,#62093,#62094,#62095,
#62096,#62097,#62098,#62099,#62100),.UNSPECIFIED.,.F.,.F.,(4,1,1,1,1,1,
1,4),(53.4070751110264,53.972191728486,54.9649029062269,55.9576140839679,
56.9503252617089,57.9430364394499,58.9357476171908,59.690260418206),
 .UNSPECIFIED.);
#1569=B_SPLINE_CURVE_WITH_KNOTS('',3,(#62105,#62106,#62107,#62108,#62109,
#62110,#62111,#62112,#62113,#62114,#62115),.UNSPECIFIED.,.F.,.F.,(4,1,1,
1,1,1,1,1,4),(47.1238898038469,47.3223749485198,48.3142455624282,49.3061161763366,
50.2979867902449,51.2898574041533,52.2817280180617,53.2735986319701,53.4070751110265),
 .UNSPECIFIED.);
#1570=B_SPLINE_CURVE_WITH_KNOTS('',3,(#62116,#62117,#62118,#62119,#62120,
#62121,#62122,#62123,#62124,#62125),.UNSPECIFIED.,.F.,.F.,(4,1,1,1,1,1,
1,4),(47.1238898038468,48.0159246620401,49.0086358397811,50.001347017522,
50.994058195263,51.986769373004,52.979480550745,53.4070751110264),
 .UNSPECIFIED.);
#1571=B_SPLINE_CURVE_WITH_KNOTS('',3,(#62130,#62131,#62132,#62133,#62134,
#62135,#62136,#62137,#62138,#62139),.UNSPECIFIED.,.F.,.F.,(4,1,1,1,1,1,
1,4),(40.8407044966673,41.3711512650695,42.3630218789779,43.3548924928863,
44.3467631067947,45.3386337207031,46.3305043346114,47.1238898038469),
 .UNSPECIFIED.);
#1572=B_SPLINE_CURVE_WITH_KNOTS('',3,(#62140,#62141,#62142,#62143,#62144,
#62145,#62146,#62147,#62148,#62149,#62150),.UNSPECIFIED.,.F.,.F.,(4,1,1,
1,1,1,1,1,4),(40.8407044966672,41.0669464178533,42.0596575955942,43.0523687733352,
44.0450799510762,45.0377911288172,46.0305023065581,47.0232134842991,47.1238898038468),
 .UNSPECIFIED.);
#1573=B_SPLINE_CURVE_WITH_KNOTS('',3,(#62155,#62156,#62157,#62158,#62159,
#62160,#62161,#62162,#62163,#62164),.UNSPECIFIED.,.F.,.F.,(4,1,1,1,1,1,
1,4),(34.5575191894877,35.4199275816193,36.4117981955277,37.403668809436,
38.3955394233444,39.3874100372528,40.3792806511612,40.8407044966673),
 .UNSPECIFIED.);
#1574=B_SPLINE_CURVE_WITH_KNOTS('',3,(#62165,#62166,#62167,#62168,#62169,
#62170,#62171,#62172,#62173,#62174),.UNSPECIFIED.,.F.,.F.,(4,1,1,1,1,1,
1,4),(34.5575191894876,35.1106793514074,36.1033905291484,37.0961017068893,
38.0888128846303,39.0815240623713,40.0742352401123,40.8407044966672),
 .UNSPECIFIED.);
#1575=B_SPLINE_CURVE_WITH_KNOTS('',3,(#62179,#62180,#62181,#62182,#62183,
#62184,#62185,#62186,#62187,#62188,#62189),.UNSPECIFIED.,.F.,.F.,(4,1,1,
1,1,1,1,1,4),(28.2743338823081,28.4768332842606,29.468703898169,30.4605745120774,
31.4524451259858,32.4443157398941,33.4361863538025,34.4280569677109,34.5575191894877),
 .UNSPECIFIED.);
#1576=B_SPLINE_CURVE_WITH_KNOTS('',3,(#62190,#62191,#62192,#62193,#62194,
#62195,#62196,#62197,#62198,#62199),.UNSPECIFIED.,.F.,.F.,(4,1,1,1,1,1,
1,4),(28.2743338823081,29.1544122849615,30.1471234627025,31.1398346404435,
32.1325458181845,33.1252569959254,34.1179681736664,34.5575191894876),
 .UNSPECIFIED.);
#1577=B_SPLINE_CURVE_WITH_KNOTS('',3,(#62204,#62205,#62206,#62207,#62208,
#62209,#62210,#62211,#62212,#62213),.UNSPECIFIED.,.F.,.F.,(4,1,1,1,1,1,
1,4),(21.9911485751285,22.5256096008104,23.5174802147187,24.5093508286271,
25.5012214425355,26.4930920564439,27.4849626703523,28.2743338823081),
 .UNSPECIFIED.);
#1578=B_SPLINE_CURVE_WITH_KNOTS('',3,(#62214,#62215,#62216,#62217,#62218,
#62219,#62220,#62221,#62222,#62223,#62224),.UNSPECIFIED.,.F.,.F.,(4,1,1,
1,1,1,1,1,4),(21.9911485751285,22.2054340407747,23.1981452185157,24.1908563962566,
25.1835675739976,26.1762787517386,27.1689899294796,28.1617011072206,28.2743338823081),
 .UNSPECIFIED.);
#1579=B_SPLINE_CURVE_WITH_KNOTS('',3,(#62229,#62230,#62231,#62232,#62233,
#62234,#62235,#62236,#62237,#62238),.UNSPECIFIED.,.F.,.F.,(4,1,1,1,1,1,
1,4),(15.7079632679489,16.5743859173601,17.5662565312685,18.5581271451769,
19.5499977590852,20.5418683729936,21.533738986902,21.9911485751285),
 .UNSPECIFIED.);
#1580=B_SPLINE_CURVE_WITH_KNOTS('',3,(#62239,#62240,#62241,#62242,#62243,
#62244,#62245,#62246,#62247,#62248),.UNSPECIFIED.,.F.,.F.,(4,1,1,1,1,1,
1,4),(15.7079632679489,16.2491669743288,17.2418781520698,18.2345893298108,
19.2273005075518,20.2200116852927,21.2127228630337,21.9911485751285),
 .UNSPECIFIED.);
#1581=B_SPLINE_CURVE_WITH_KNOTS('',3,(#62251,#62252,#62253,#62254,#62255,
#62256,#62257,#62258,#62259,#62260,#62261,#62262,#62263,#62264,#62265,#62266,
#62267,#62268,#62269,#62270,#62271,#62272,#62273,#62274,#62275,#62276,#62277,
#62278,#62279,#62280,#62281,#62282,#62283,#62284,#62285,#62286,#62287,#62288,
#62289,#62290,#62291,#62292,#62293,#62294,#62295,#62296,#62297,#62298,#62299,
#62300,#62301,#62302,#62303,#62304,#62305,#62306,#62307,#62308,#62309,#62310,
#62311,#62312,#62313,#62314,#62315,#62316,#62317,#62318,#62319,#62320,#62321,
#62322,#62323,#62324,#62325,#62326,#62327,#62328,#62329,#62330,#62331,#62332,
#62333,#62334,#62335,#62336,#62337,#62338,#62339,#62340,#62341,#62342,#62343,
#62344,#62345,#62346,#62347,#62348,#62349,#62350,#62351,#62352,#62353,#62354,
#62355,#62356,#62357,#62358,#62359,#62360,#62361,#62362,#62363,#62364,#62365,
#62366,#62367,#62368,#62369,#62370,#62371,#62372,#62373,#62374,#62375,#62376,
#62377,#62378,#62379,#62380,#62381,#62382,#62383,#62384,#62385,#62386,#62387,
#62388,#62389,#62390,#62391,#62392,#62393,#62394,#62395,#62396,#62397,#62398,
#62399,#62400,#62401,#62402,#62403,#62404,#62405,#62406,#62407,#62408,#62409,
#62410,#62411,#62412,#62413,#62414,#62415,#62416,#62417,#62418,#62419,#62420,
#62421,#62422,#62423,#62424,#62425,#62426,#62427,#62428,#62429,#62430,#62431,
#62432,#62433,#62434,#62435,#62436,#62437,#62438,#62439,#62440,#62441,#62442,
#62443,#62444,#62445,#62446,#62447,#62448,#62449,#62450,#62451,#62452,#62453,
#62454,#62455,#62456,#62457,#62458,#62459,#62460,#62461,#62462,#62463,#62464,
#62465,#62466,#62467,#62468,#62469,#62470),.UNSPECIFIED.,.F.,.F.,(4,3,3,
3,3,3,3,3,3,3,3,3,3,3,3,3,3,3,3,3,3,3,3,3,3,3,3,3,3,3,3,3,3,3,3,3,3,3,3,
3,3,3,3,3,3,3,3,3,3,3,3,3,3,3,3,3,3,3,3,3,3,3,3,3,3,3,3,3,3,3,3,3,3,4),
(-1.5115530493723,-1.48679433039677,-1.46137997144481,-1.44936627203976,
-1.44203978844916,-1.43723948275662,-1.41130482704604,-1.3851425648951,
-1.36907979899106,-1.36528335260342,-1.33883417182409,-1.31251413265359,
-1.29083745680875,-1.27999911888633,-1.27252822943752,-1.26916078096391,
-1.2438409010096,-1.21777622976252,-1.19264806966918,-1.18165449962834,
-1.17500808302858,-1.17140113753098,-1.14461626345551,-1.11752388424601,
-1.09233065043846,-1.08197947093734,-1.07663416157974,-1.07221334700158,
-1.04448214800868,-1.01675094901579,-0.989899829038698,-0.980534050538336,
-0.975142748268706,-0.971473262423844,-0.944367339171939,-0.916829945945447,
-0.889160172398661,-0.878253059899969,-0.87283587922991,-0.869128423226553,
-0.840502786522066,-0.812629809126308,-0.785184824902654,-0.776260550181423,
-0.769615191493828,-0.76539079696697,-0.754625876408607,-0.727617533495154,
-0.699889836956671,-0.672733437279935,-0.663027286995113,-0.658922109894078,
-0.630659562625353,-0.602060824740566,-0.57220527844112,-0.560770556686858,
-0.556383058918736,-0.552005977862112,-0.523133364911618,-0.494697204184849,
-0.482638639542781,-0.454174910522506,-0.448377858002803,-0.443883394073885,
-0.415482165359649,-0.386508614853008,-0.357316612716015,-0.340170191390177,
-0.335377465438287,-0.305918315871394,-0.27645436453335,-0.247645675491356,
-0.226999958751525,-0.219677966288016),.UNSPECIFIED.);
#1582=B_SPLINE_CURVE_WITH_KNOTS('',3,(#62472,#62473,#62474,#62475,#62476,
#62477,#62478,#62479,#62480,#62481,#62482,#62483,#62484,#62485,#62486,#62487,
#62488,#62489,#62490,#62491,#62492,#62493,#62494,#62495,#62496,#62497,#62498,
#62499,#62500,#62501,#62502,#62503,#62504,#62505,#62506,#62507,#62508,#62509,
#62510,#62511,#62512,#62513,#62514,#62515,#62516,#62517,#62518,#62519,#62520,
#62521,#62522,#62523,#62524,#62525,#62526,#62527,#62528,#62529,#62530,#62531,
#62532,#62533,#62534,#62535),.UNSPECIFIED.,.F.,.F.,(4,3,3,3,3,3,3,3,3,3,
3,3,3,3,3,3,3,3,3,3,3,4),(-0.410648750433038,-0.381296088292737,-0.350882391849445,
-0.328072119516976,-0.310964415267624,-0.305842993500878,-0.301661871504881,
-0.274116258800685,-0.259641302519569,-0.231392457082299,-0.202468399947011,
-0.198019208917011,-0.170841895434807,-0.143725312403613,-0.117042212888725,
-0.102411936277635,-0.097195049751494,-0.0935363835720784,-0.0677899334604712,
-0.0424347820407558,-0.0178142542830924,0.),.UNSPECIFIED.);
#1583=B_SPLINE_CURVE_WITH_KNOTS('',3,(#62538,#62539,#62540,#62541,#62542,
#62543,#62544,#62545,#62546,#62547,#62548,#62549,#62550,#62551,#62552,#62553,
#62554,#62555,#62556,#62557,#62558,#62559,#62560,#62561,#62562,#62563,#62564,
#62565,#62566,#62567,#62568),.UNSPECIFIED.,.F.,.F.,(4,3,3,3,3,3,3,3,3,3,
4),(-0.219677966288016,-0.201006229477425,-0.172158028090248,-0.142713390739092,
-0.124874216896705,-0.114789665948937,-0.110082687886506,-0.0803547102951982,
-0.0502957032480209,-0.0203907630638487,0.),.UNSPECIFIED.);
#1584=B_SPLINE_CURVE_WITH_KNOTS('',3,(#62981,#62982,#62983,#62984,#62985,
#62986,#62987,#62988),.UNSPECIFIED.,.F.,.F.,(4,1,1,1,1,4),(11.6150328478182,
12.6069034617266,13.598774075635,14.5906446895433,15.5825153034517,15.7079632679489),
 .UNSPECIFIED.);
#1585=B_SPLINE_CURVE_WITH_KNOTS('',3,(#62989,#62990,#62991,#62992,#62993,
#62994,#62995,#62996,#62997,#62998,#62999,#63000,#63001,#63002,#63003,#63004,
#63005,#63006,#63007,#63008,#63009,#63010,#63011,#63012,#63013,#63014,#63015,
#63016,#63017,#63018,#63019,#63020,#63021,#63022,#63023,#63024,#63025,#63026,
#63027,#63028,#63029,#63030,#63031,#63032,#63033,#63034,#63035,#63036,#63037,
#63038,#63039,#63040,#63041,#63042,#63043,#63044,#63045,#63046,#63047,#63048,
#63049,#63050,#63051,#63052,#63053,#63054,#63055,#63056,#63057,#63058,#63059,
#63060,#63061,#63062,#63063,#63064,#63065,#63066,#63067,#63068,#63069,#63070,
#63071,#63072,#63073,#63074,#63075,#63076),.UNSPECIFIED.,.F.,.F.,(4,3,3,
3,3,3,3,3,3,3,3,3,3,3,3,3,3,3,3,3,3,3,3,3,3,3,3,3,3,4),(-0.552745378375041,
-0.527830263536694,-0.498419933292456,-0.482944277728704,-0.477004703287069,
-0.471889411648522,-0.442842142020847,-0.418838054802294,-0.408336266644177,
-0.40199148464016,-0.397446251891128,-0.369139848009071,-0.341087780585202,
-0.313931322984348,-0.298150853306366,-0.293754274173184,-0.266922432864957,
-0.250809444272419,-0.223433348051691,-0.19550417954523,-0.19139998392206,
-0.164790719651446,-0.138164593558308,-0.11192170155777,-0.0979314888630491,
-0.0936568444848153,-0.0680692021908508,-0.0428602319276656,-0.0184469101431373,
0.),.UNSPECIFIED.);
#1586=B_SPLINE_CURVE_WITH_KNOTS('',3,(#63077,#63078,#63079,#63080,#63081,
#63082,#63083,#63084,#63085,#63086,#63087,#63088,#63089,#63090,#63091,#63092,
#63093,#63094,#63095),.UNSPECIFIED.,.F.,.F.,(4,3,3,3,3,3,4),(-96.6808425304193,
-96.2114495491126,-95.2195789352043,-94.2277083212959,-93.2358377073875,
-92.2439670934791,-92.0575247206449),.UNSPECIFIED.);
#1587=B_SPLINE_CURVE_WITH_KNOTS('',3,(#63098,#63099,#63100,#63101,#63102,
#63103,#63104,#63105,#63106),.UNSPECIFIED.,.F.,.F.,(4,1,1,1,1,1,4),(10.3761157273101,
11.2856110856239,12.2783222633649,13.2710334411059,14.2637446188469,15.2564557965878,
15.7079632679489),.UNSPECIFIED.);
#1588=B_SPLINE_CURVE_WITH_KNOTS('',3,(#63524,#63525,#63526,#63527,#63528,
#63529,#63530,#63531,#63532,#63533,#63534,#63535,#63536,#63537,#63538,#63539,
#63540,#63541,#63542,#63543,#63544,#63545),.UNSPECIFIED.,.F.,.F.,(4,3,3,
3,3,3,3,4),(89.0818947088825,89.3440059966879,90.3367171744289,91.3294283521699,
92.3221395299109,93.3148507076518,94.3075618853928,94.6122043555102),
 .UNSPECIFIED.);
#1589=B_SPLINE_CURVE_WITH_KNOTS('',3,(#63546,#63547,#63548,#63549,#63550,
#63551,#63552,#63553,#63554,#63555,#63556,#63557,#63558,#63559,#63560,#63561,
#63562,#63563,#63564,#63565,#63566,#63567,#63568,#63569,#63570,#63571,#63572,
#63573,#63574,#63575,#63576,#63577,#63578,#63579,#63580,#63581,#63582,#63583,
#63584,#63585,#63586,#63587,#63588,#63589,#63590,#63591,#63592,#63593,#63594,
#63595,#63596,#63597,#63598,#63599,#63600,#63601,#63602,#63603,#63604,#63605,
#63606,#63607,#63608,#63609,#63610,#63611,#63612,#63613,#63614,#63615,#63616,
#63617,#63618,#63619,#63620,#63621,#63622,#63623,#63624,#63625,#63626,#63627,
#63628,#63629,#63630,#63631,#63632,#63633),.UNSPECIFIED.,.F.,.F.,(4,3,3,
3,3,3,3,3,3,3,3,3,3,3,3,3,3,3,3,3,3,3,3,3,3,3,3,3,3,4),(-0.555272788399392,
-0.535208229286056,-0.51046000550438,-0.495927663091087,-0.490771565699598,
-0.464551573131573,-0.44160907963455,-0.431518091480653,-0.425427657470475,
-0.420791193383041,-0.394188077983384,-0.365893964776387,-0.344673379871139,
-0.328757941192203,-0.324434111993057,-0.296521822210165,-0.281011625155395,
-0.254049889550291,-0.226554106924644,-0.220947145848259,-0.216688100237889,
-0.188737539857684,-0.160250957640402,-0.131525362881473,-0.114279480489655,
-0.109581292141837,-0.0801117384511396,-0.0505679692714886,-0.0215915474943119,
0.),.UNSPECIFIED.);
#2141=CYLINDRICAL_SURFACE('',#15435,2.942);
#2142=CYLINDRICAL_SURFACE('',#15437,2.942);
#2143=CYLINDRICAL_SURFACE('',#15438,2.942);
#2144=CYLINDRICAL_SURFACE('',#15439,2.942);
#2145=CYLINDRICAL_SURFACE('',#15440,2.942);
#2146=CYLINDRICAL_SURFACE('',#15441,2.942);
#2147=CYLINDRICAL_SURFACE('',#15442,2.942);
#2148=CYLINDRICAL_SURFACE('',#15443,2.942);
#2149=CYLINDRICAL_SURFACE('',#15444,2.942);
#2150=CYLINDRICAL_SURFACE('',#15445,2.942);
#2151=CYLINDRICAL_SURFACE('',#15446,2.942);
#2152=CYLINDRICAL_SURFACE('',#15447,2.942);
#2153=CYLINDRICAL_SURFACE('',#15448,2.942);
#2154=CYLINDRICAL_SURFACE('',#15449,2.942);
#2155=CYLINDRICAL_SURFACE('',#15450,2.942);
#2156=CYLINDRICAL_SURFACE('',#15451,2.37175);
#2157=CYLINDRICAL_SURFACE('',#15453,2.37175);
#2158=CYLINDRICAL_SURFACE('',#15454,2.37175);
#2159=CYLINDRICAL_SURFACE('',#15455,2.37175);
#2160=CYLINDRICAL_SURFACE('',#15456,2.37175);
#2161=CYLINDRICAL_SURFACE('',#15457,2.37175);
#2162=CYLINDRICAL_SURFACE('',#15458,2.37175);
#2163=CYLINDRICAL_SURFACE('',#15459,2.37175);
#2164=CYLINDRICAL_SURFACE('',#15460,2.37175);
#2165=CYLINDRICAL_SURFACE('',#15461,2.37175);
#2166=CYLINDRICAL_SURFACE('',#15462,2.37175);
#2167=CYLINDRICAL_SURFACE('',#15463,2.37175);
#2168=CYLINDRICAL_SURFACE('',#15464,2.37175);
#2169=CYLINDRICAL_SURFACE('',#15465,2.37175);
#2170=CYLINDRICAL_SURFACE('',#15466,2.37175);
#2171=CYLINDRICAL_SURFACE('',#15470,2.37175);
#2172=CYLINDRICAL_SURFACE('',#15472,2.942);
#2173=CYLINDRICAL_SURFACE('',#15482,5.);
#2190=SHAPE_REPRESENTATION_RELATIONSHIP('SRR','None',#63875,#2206);
#2206=ADVANCED_BREP_SHAPE_REPRESENTATION('',(#2238),#63753);
#2222=STYLED_ITEM('',(#63960),#2238);
#2238=MANIFOLD_SOLID_BREP('Body1',#14323);
#2299=FACE_BOUND('',#3875,.T.);
#2300=FACE_BOUND('',#3878,.T.);
#3013=FACE_OUTER_BOUND('',#3832,.T.);
#3014=FACE_OUTER_BOUND('',#3833,.T.);
#3015=FACE_OUTER_BOUND('',#3834,.T.);
#3016=FACE_OUTER_BOUND('',#3835,.T.);
#3017=FACE_OUTER_BOUND('',#3836,.T.);
#3018=FACE_OUTER_BOUND('',#3837,.T.);
#3019=FACE_OUTER_BOUND('',#3838,.T.);
#3020=FACE_OUTER_BOUND('',#3839,.T.);
#3021=FACE_OUTER_BOUND('',#3840,.T.);
#3022=FACE_OUTER_BOUND('',#3841,.T.);
#3023=FACE_OUTER_BOUND('',#3842,.T.);
#3024=FACE_OUTER_BOUND('',#3843,.T.);
#3025=FACE_OUTER_BOUND('',#3844,.T.);
#3026=FACE_OUTER_BOUND('',#3845,.T.);
#3027=FACE_OUTER_BOUND('',#3846,.T.);
#3028=FACE_OUTER_BOUND('',#3847,.T.);
#3029=FACE_OUTER_BOUND('',#3848,.T.);
#3030=FACE_OUTER_BOUND('',#3849,.T.);
#3031=FACE_OUTER_BOUND('',#3850,.T.);
#3032=FACE_OUTER_BOUND('',#3851,.T.);
#3033=FACE_OUTER_BOUND('',#3852,.T.);
#3034=FACE_OUTER_BOUND('',#3853,.T.);
#3035=FACE_OUTER_BOUND('',#3854,.T.);
#3036=FACE_OUTER_BOUND('',#3855,.T.);
#3037=FACE_OUTER_BOUND('',#3856,.T.);
#3038=FACE_OUTER_BOUND('',#3857,.T.);
#3039=FACE_OUTER_BOUND('',#3858,.T.);
#3040=FACE_OUTER_BOUND('',#3859,.T.);
#3041=FACE_OUTER_BOUND('',#3860,.T.);
#3042=FACE_OUTER_BOUND('',#3861,.T.);
#3043=FACE_OUTER_BOUND('',#3862,.T.);
#3044=FACE_OUTER_BOUND('',#3863,.T.);
#3045=FACE_OUTER_BOUND('',#3864,.T.);
#3046=FACE_OUTER_BOUND('',#3865,.T.);
#3047=FACE_OUTER_BOUND('',#3866,.T.);
#3048=FACE_OUTER_BOUND('',#3867,.T.);
#3049=FACE_OUTER_BOUND('',#3868,.T.);
#3050=FACE_OUTER_BOUND('',#3869,.T.);
#3051=FACE_OUTER_BOUND('',#3870,.T.);
#3052=FACE_OUTER_BOUND('',#3871,.T.);
#3053=FACE_OUTER_BOUND('',#3872,.T.);
#3054=FACE_OUTER_BOUND('',#3873,.T.);
#3055=FACE_OUTER_BOUND('',#3874,.T.);
#3056=FACE_OUTER_BOUND('',#3876,.T.);
#3057=FACE_OUTER_BOUND('',#3877,.T.);
#3058=FACE_OUTER_BOUND('',#3879,.T.);
#3832=EDGE_LOOP('',(#13145,#13146,#13147,#13148));
#3833=EDGE_LOOP('',(#13149,#13150,#13151,#13152));
#3834=EDGE_LOOP('',(#13153,#13154,#13155,#13156));
#3835=EDGE_LOOP('',(#13157,#13158,#13159,#13160));
#3836=EDGE_LOOP('',(#13161,#13162,#13163,#13164));
#3837=EDGE_LOOP('',(#13165,#13166,#13167,#13168));
#3838=EDGE_LOOP('',(#13169,#13170,#13171,#13172));
#3839=EDGE_LOOP('',(#13173,#13174,#13175,#13176));
#3840=EDGE_LOOP('',(#13177,#13178,#13179,#13180));
#3841=EDGE_LOOP('',(#13181,#13182,#13183,#13184));
#3842=EDGE_LOOP('',(#13185,#13186,#13187,#13188));
#3843=EDGE_LOOP('',(#13189,#13190,#13191,#13192));
#3844=EDGE_LOOP('',(#13193,#13194,#13195,#13196));
#3845=EDGE_LOOP('',(#13197,#13198,#13199,#13200));
#3846=EDGE_LOOP('',(#13201,#13202,#13203,#13204));
#3847=EDGE_LOOP('',(#13205,#13206,#13207,#13208));
#3848=EDGE_LOOP('',(#13209,#13210,#13211,#13212));
#3849=EDGE_LOOP('',(#13213,#13214,#13215,#13216));
#3850=EDGE_LOOP('',(#13217,#13218,#13219,#13220));
#3851=EDGE_LOOP('',(#13221,#13222,#13223,#13224));
#3852=EDGE_LOOP('',(#13225,#13226,#13227,#13228));
#3853=EDGE_LOOP('',(#13229,#13230,#13231,#13232));
#3854=EDGE_LOOP('',(#13233,#13234,#13235,#13236));
#3855=EDGE_LOOP('',(#13237,#13238,#13239,#13240));
#3856=EDGE_LOOP('',(#13241,#13242,#13243,#13244));
#3857=EDGE_LOOP('',(#13245,#13246,#13247,#13248));
#3858=EDGE_LOOP('',(#13249,#13250,#13251,#13252));
#3859=EDGE_LOOP('',(#13253,#13254,#13255,#13256));
#3860=EDGE_LOOP('',(#13257,#13258,#13259,#13260));
#3861=EDGE_LOOP('',(#13261,#13262,#13263,#13264));
#3862=EDGE_LOOP('',(#13265,#13266,#13267,#13268,#13269,#13270,#13271,#13272));
#3863=EDGE_LOOP('',(#13273,#13274,#13275,#13276,#13277,#13278,#13279,#13280,
#13281,#13282,#13283,#13284,#13285,#13286,#13287,#13288,#13289,#13290,#13291,
#13292,#13293,#13294,#13295,#13296,#13297,#13298,#13299,#13300,#13301,#13302,
#13303,#13304,#13305,#13306));
#3864=EDGE_LOOP('',(#13307,#13308,#13309,#13310));
#3865=EDGE_LOOP('',(#13311,#13312,#13313,#13314,#13315,#13316,#13317,#13318,
#13319,#13320,#13321,#13322,#13323,#13324,#13325,#13326,#13327,#13328,#13329,
#13330,#13331,#13332,#13333,#13334,#13335,#13336,#13337,#13338,#13339,#13340,
#13341,#13342,#13343,#13344,#13345));
#3866=EDGE_LOOP('',(#13346,#13347,#13348,#13349));
#3867=EDGE_LOOP('',(#13350,#13351,#13352,#13353));
#3868=EDGE_LOOP('',(#13354,#13355,#13356,#13357));
#3869=EDGE_LOOP('',(#13358,#13359,#13360,#13361));
#3870=EDGE_LOOP('',(#13362,#13363,#13364,#13365));
#3871=EDGE_LOOP('',(#13366,#13367,#13368,#13369));
#3872=EDGE_LOOP('',(#13370,#13371,#13372,#13373));
#3873=EDGE_LOOP('',(#13374,#13375,#13376,#13377,#13378,#13379));
#3874=EDGE_LOOP('',(#13380));
#3875=EDGE_LOOP('',(#13381,#13382,#13383,#13384));
#3876=EDGE_LOOP('',(#13385,#13386,#13387,#13388));
#3877=EDGE_LOOP('',(#13389));
#3878=EDGE_LOOP('',(#13390,#13391,#13392,#13393,#13394,#13395));
#3879=EDGE_LOOP('',(#13396));
#4670=LINE('',#61162,#5506);
#4671=LINE('',#61186,#5507);
#4672=LINE('',#61234,#5508);
#4673=LINE('',#61282,#5509);
#4674=LINE('',#61336,#5510);
#4675=LINE('',#61384,#5511);
#4676=LINE('',#61432,#5512);
#4677=LINE('',#61486,#5513);
#4678=LINE('',#61534,#5514);
#4679=LINE('',#61582,#5515);
#4680=LINE('',#61636,#5516);
#4681=LINE('',#61684,#5517);
#4682=LINE('',#61732,#5518);
#4683=LINE('',#61786,#5519);
#4684=LINE('',#61834,#5520);
#4685=LINE('',#61882,#5521);
#4686=LINE('',#61907,#5522);
#4687=LINE('',#61932,#5523);
#4688=LINE('',#61956,#5524);
#4689=LINE('',#61981,#5525);
#4690=LINE('',#62006,#5526);
#4691=LINE('',#62030,#5527);
#4692=LINE('',#62055,#5528);
#4693=LINE('',#62080,#5529);
#4694=LINE('',#62104,#5530);
#4695=LINE('',#62129,#5531);
#4696=LINE('',#62154,#5532);
#4697=LINE('',#62178,#5533);
#4698=LINE('',#62203,#5534);
#4699=LINE('',#62228,#5535);
#4700=LINE('',#62570,#5536);
#4701=LINE('',#63638,#5537);
#4702=LINE('',#63640,#5538);
#4703=LINE('',#63642,#5539);
#4704=LINE('',#63643,#5540);
#4705=LINE('',#63646,#5541);
#4706=LINE('',#63648,#5542);
#4707=LINE('',#63649,#5543);
#4708=LINE('',#63652,#5544);
#4709=LINE('',#63654,#5545);
#4710=LINE('',#63655,#5546);
#4711=LINE('',#63658,#5547);
#4712=LINE('',#63660,#5548);
#4713=LINE('',#63661,#5549);
#4714=LINE('',#63664,#5550);
#4715=LINE('',#63666,#5551);
#4716=LINE('',#63667,#5552);
#4717=LINE('',#63669,#5553);
#4718=LINE('',#63670,#5554);
#4719=LINE('',#63677,#5555);
#5506=VECTOR('',#18167,3.);
#5507=VECTOR('',#18172,3.);
#5508=VECTOR('',#18175,3.);
#5509=VECTOR('',#18178,3.);
#5510=VECTOR('',#18181,3.);
#5511=VECTOR('',#18184,3.);
#5512=VECTOR('',#18187,3.);
#5513=VECTOR('',#18190,3.);
#5514=VECTOR('',#18193,3.);
#5515=VECTOR('',#18196,3.);
#5516=VECTOR('',#18199,3.);
#5517=VECTOR('',#18202,3.);
#5518=VECTOR('',#18205,3.);
#5519=VECTOR('',#18208,3.);
#5520=VECTOR('',#18211,3.);
#5521=VECTOR('',#18214,2.37175);
#5522=VECTOR('',#18219,2.37175);
#5523=VECTOR('',#18222,2.37175);
#5524=VECTOR('',#18225,2.37175);
#5525=VECTOR('',#18228,2.37175);
#5526=VECTOR('',#18231,2.37175);
#5527=VECTOR('',#18234,2.37175);
#5528=VECTOR('',#18237,2.37175);
#5529=VECTOR('',#18240,2.37175);
#5530=VECTOR('',#18243,2.37175);
#5531=VECTOR('',#18246,2.37175);
#5532=VECTOR('',#18249,2.37175);
#5533=VECTOR('',#18252,2.37175);
#5534=VECTOR('',#18255,2.37175);
#5535=VECTOR('',#18258,2.37175);
#5536=VECTOR('',#18263,2.5);
#5537=VECTOR('',#18274,10.);
#5538=VECTOR('',#18275,10.);
#5539=VECTOR('',#18276,10.);
#5540=VECTOR('',#18277,10.);
#5541=VECTOR('',#18280,10.);
#5542=VECTOR('',#18281,10.);
#5543=VECTOR('',#18282,10.);
#5544=VECTOR('',#18285,10.);
#5545=VECTOR('',#18286,10.);
#5546=VECTOR('',#18287,10.);
#5547=VECTOR('',#18290,10.);
#5548=VECTOR('',#18291,10.);
#5549=VECTOR('',#18292,10.);
#5550=VECTOR('',#18295,10.);
#5551=VECTOR('',#18296,10.);
#5552=VECTOR('',#18297,10.);
#5553=VECTOR('',#18300,10.);
#5554=VECTOR('',#18301,10.);
#5555=VECTOR('',#18310,5.);
#6898=VERTEX_POINT('',#61160);
#6899=VERTEX_POINT('',#61161);
#6900=VERTEX_POINT('',#61163);
#6901=VERTEX_POINT('',#61174);
#6902=VERTEX_POINT('',#61184);
#6903=VERTEX_POINT('',#61185);
#6904=VERTEX_POINT('',#61232);
#6905=VERTEX_POINT('',#61233);
#6906=VERTEX_POINT('',#61280);
#6907=VERTEX_POINT('',#61281);
#6908=VERTEX_POINT('',#61334);
#6909=VERTEX_POINT('',#61335);
#6910=VERTEX_POINT('',#61382);
#6911=VERTEX_POINT('',#61383);
#6912=VERTEX_POINT('',#61430);
#6913=VERTEX_POINT('',#61431);
#6914=VERTEX_POINT('',#61484);
#6915=VERTEX_POINT('',#61485);
#6916=VERTEX_POINT('',#61532);
#6917=VERTEX_POINT('',#61533);
#6918=VERTEX_POINT('',#61580);
#6919=VERTEX_POINT('',#61581);
#6920=VERTEX_POINT('',#61634);
#6921=VERTEX_POINT('',#61635);
#6922=VERTEX_POINT('',#61682);
#6923=VERTEX_POINT('',#61683);
#6924=VERTEX_POINT('',#61730);
#6925=VERTEX_POINT('',#61731);
#6926=VERTEX_POINT('',#61784);
#6927=VERTEX_POINT('',#61785);
#6928=VERTEX_POINT('',#61832);
#6929=VERTEX_POINT('',#61833);
#6930=VERTEX_POINT('',#61880);
#6931=VERTEX_POINT('',#61881);
#6932=VERTEX_POINT('',#61883);
#6933=VERTEX_POINT('',#61894);
#6934=VERTEX_POINT('',#61905);
#6935=VERTEX_POINT('',#61906);
#6936=VERTEX_POINT('',#61930);
#6937=VERTEX_POINT('',#61931);
#6938=VERTEX_POINT('',#61954);
#6939=VERTEX_POINT('',#61955);
#6940=VERTEX_POINT('',#61979);
#6941=VERTEX_POINT('',#61980);
#6942=VERTEX_POINT('',#62004);
#6943=VERTEX_POINT('',#62005);
#6944=VERTEX_POINT('',#62028);
#6945=VERTEX_POINT('',#62029);
#6946=VERTEX_POINT('',#62053);
#6947=VERTEX_POINT('',#62054);
#6948=VERTEX_POINT('',#62078);
#6949=VERTEX_POINT('',#62079);
#6950=VERTEX_POINT('',#62102);
#6951=VERTEX_POINT('',#62103);
#6952=VERTEX_POINT('',#62127);
#6953=VERTEX_POINT('',#62128);
#6954=VERTEX_POINT('',#62152);
#6955=VERTEX_POINT('',#62153);
#6956=VERTEX_POINT('',#62176);
#6957=VERTEX_POINT('',#62177);
#6958=VERTEX_POINT('',#62201);
#6959=VERTEX_POINT('',#62202);
#6960=VERTEX_POINT('',#62226);
#6961=VERTEX_POINT('',#62227);
#6962=VERTEX_POINT('',#62250);
#6963=VERTEX_POINT('',#62471);
#6964=VERTEX_POINT('',#62536);
#6965=VERTEX_POINT('',#62569);
#6966=VERTEX_POINT('',#62980);
#6967=VERTEX_POINT('',#63097);
#6968=VERTEX_POINT('',#63636);
#6969=VERTEX_POINT('',#63637);
#6970=VERTEX_POINT('',#63639);
#6971=VERTEX_POINT('',#63641);
#6972=VERTEX_POINT('',#63645);
#6973=VERTEX_POINT('',#63647);
#6974=VERTEX_POINT('',#63651);
#6975=VERTEX_POINT('',#63653);
#6976=VERTEX_POINT('',#63657);
#6977=VERTEX_POINT('',#63659);
#6978=VERTEX_POINT('',#63663);
#6979=VERTEX_POINT('',#63665);
#6980=VERTEX_POINT('',#63673);
#6981=VERTEX_POINT('',#63676);
#8995=EDGE_CURVE('',#6898,#6899,#4670,.T.);
#8996=EDGE_CURVE('',#6898,#6900,#1521,.T.);
#8997=EDGE_CURVE('',#6900,#6901,#476,.F.);
#8998=EDGE_CURVE('',#6901,#6899,#1522,.T.);
#8999=EDGE_CURVE('',#6902,#6903,#4671,.T.);
#9000=EDGE_CURVE('',#6902,#6898,#1523,.T.);
#9001=EDGE_CURVE('',#6899,#6903,#1524,.T.);
#9002=EDGE_CURVE('',#6904,#6905,#4672,.T.);
#9003=EDGE_CURVE('',#6904,#6902,#1525,.T.);
#9004=EDGE_CURVE('',#6903,#6905,#1526,.T.);
#9005=EDGE_CURVE('',#6906,#6907,#4673,.T.);
#9006=EDGE_CURVE('',#6906,#6904,#1527,.T.);
#9007=EDGE_CURVE('',#6905,#6907,#1528,.T.);
#9008=EDGE_CURVE('',#6908,#6909,#4674,.T.);
#9009=EDGE_CURVE('',#6908,#6906,#1529,.T.);
#9010=EDGE_CURVE('',#6907,#6909,#1530,.T.);
#9011=EDGE_CURVE('',#6910,#6911,#4675,.T.);
#9012=EDGE_CURVE('',#6910,#6908,#1531,.T.);
#9013=EDGE_CURVE('',#6909,#6911,#1532,.T.);
#9014=EDGE_CURVE('',#6912,#6913,#4676,.T.);
#9015=EDGE_CURVE('',#6912,#6910,#1533,.T.);
#9016=EDGE_CURVE('',#6911,#6913,#1534,.T.);
#9017=EDGE_CURVE('',#6914,#6915,#4677,.T.);
#9018=EDGE_CURVE('',#6914,#6912,#1535,.T.);
#9019=EDGE_CURVE('',#6913,#6915,#1536,.T.);
#9020=EDGE_CURVE('',#6916,#6917,#4678,.T.);
#9021=EDGE_CURVE('',#6916,#6914,#1537,.T.);
#9022=EDGE_CURVE('',#6915,#6917,#1538,.T.);
#9023=EDGE_CURVE('',#6918,#6919,#4679,.T.);
#9024=EDGE_CURVE('',#6918,#6916,#1539,.T.);
#9025=EDGE_CURVE('',#6917,#6919,#1540,.T.);
#9026=EDGE_CURVE('',#6920,#6921,#4680,.T.);
#9027=EDGE_CURVE('',#6920,#6918,#1541,.T.);
#9028=EDGE_CURVE('',#6919,#6921,#1542,.T.);
#9029=EDGE_CURVE('',#6922,#6923,#4681,.T.);
#9030=EDGE_CURVE('',#6922,#6920,#1543,.T.);
#9031=EDGE_CURVE('',#6921,#6923,#1544,.T.);
#9032=EDGE_CURVE('',#6924,#6925,#4682,.T.);
#9033=EDGE_CURVE('',#6924,#6922,#1545,.T.);
#9034=EDGE_CURVE('',#6923,#6925,#1546,.T.);
#9035=EDGE_CURVE('',#6926,#6927,#4683,.T.);
#9036=EDGE_CURVE('',#6926,#6924,#1547,.T.);
#9037=EDGE_CURVE('',#6925,#6927,#1548,.T.);
#9038=EDGE_CURVE('',#6928,#6929,#4684,.T.);
#9039=EDGE_CURVE('',#6928,#6926,#1549,.T.);
#9040=EDGE_CURVE('',#6927,#6929,#1550,.T.);
#9041=EDGE_CURVE('',#6930,#6931,#4685,.T.);
#9042=EDGE_CURVE('',#6930,#6932,#1551,.T.);
#9043=EDGE_CURVE('',#6932,#6933,#477,.T.);
#9044=EDGE_CURVE('',#6931,#6933,#1552,.T.);
#9045=EDGE_CURVE('',#6934,#6935,#4686,.T.);
#9046=EDGE_CURVE('',#6934,#6930,#1553,.T.);
#9047=EDGE_CURVE('',#6935,#6931,#1554,.T.);
#9048=EDGE_CURVE('',#6936,#6937,#4687,.T.);
#9049=EDGE_CURVE('',#6936,#6934,#1555,.T.);
#9050=EDGE_CURVE('',#6937,#6935,#1556,.T.);
#9051=EDGE_CURVE('',#6938,#6939,#4688,.T.);
#9052=EDGE_CURVE('',#6938,#6936,#1557,.T.);
#9053=EDGE_CURVE('',#6939,#6937,#1558,.T.);
#9054=EDGE_CURVE('',#6940,#6941,#4689,.T.);
#9055=EDGE_CURVE('',#6940,#6938,#1559,.T.);
#9056=EDGE_CURVE('',#6941,#6939,#1560,.T.);
#9057=EDGE_CURVE('',#6942,#6943,#4690,.T.);
#9058=EDGE_CURVE('',#6942,#6940,#1561,.T.);
#9059=EDGE_CURVE('',#6943,#6941,#1562,.T.);
#9060=EDGE_CURVE('',#6944,#6945,#4691,.T.);
#9061=EDGE_CURVE('',#6944,#6942,#1563,.T.);
#9062=EDGE_CURVE('',#6945,#6943,#1564,.T.);
#9063=EDGE_CURVE('',#6946,#6947,#4692,.T.);
#9064=EDGE_CURVE('',#6946,#6944,#1565,.T.);
#9065=EDGE_CURVE('',#6947,#6945,#1566,.T.);
#9066=EDGE_CURVE('',#6948,#6949,#4693,.T.);
#9067=EDGE_CURVE('',#6948,#6946,#1567,.T.);
#9068=EDGE_CURVE('',#6949,#6947,#1568,.T.);
#9069=EDGE_CURVE('',#6950,#6951,#4694,.T.);
#9070=EDGE_CURVE('',#6950,#6948,#1569,.T.);
#9071=EDGE_CURVE('',#6951,#6949,#1570,.T.);
#9072=EDGE_CURVE('',#6952,#6953,#4695,.T.);
#9073=EDGE_CURVE('',#6952,#6950,#1571,.T.);
#9074=EDGE_CURVE('',#6953,#6951,#1572,.T.);
#9075=EDGE_CURVE('',#6954,#6955,#4696,.T.);
#9076=EDGE_CURVE('',#6954,#6952,#1573,.T.);
#9077=EDGE_CURVE('',#6955,#6953,#1574,.T.);
#9078=EDGE_CURVE('',#6956,#6957,#4697,.T.);
#9079=EDGE_CURVE('',#6956,#6954,#1575,.T.);
#9080=EDGE_CURVE('',#6957,#6955,#1576,.T.);
#9081=EDGE_CURVE('',#6958,#6959,#4698,.T.);
#9082=EDGE_CURVE('',#6958,#6956,#1577,.T.);
#9083=EDGE_CURVE('',#6959,#6957,#1578,.T.);
#9084=EDGE_CURVE('',#6960,#6961,#4699,.T.);
#9085=EDGE_CURVE('',#6960,#6958,#1579,.T.);
#9086=EDGE_CURVE('',#6961,#6959,#1580,.T.);
#9087=EDGE_CURVE('',#6933,#6962,#1581,.T.);
#9088=EDGE_CURVE('',#6963,#6932,#1582,.T.);
#9089=EDGE_CURVE('',#6964,#6963,#478,.T.);
#9090=EDGE_CURVE('',#6962,#6964,#1583,.T.);
#9091=EDGE_CURVE('',#6962,#6965,#4700,.T.);
#9092=EDGE_CURVE('',#6965,#6965,#479,.T.);
#9093=EDGE_CURVE('',#6966,#6960,#1584,.T.);
#9094=EDGE_CURVE('',#6900,#6966,#1585,.T.);
#9095=EDGE_CURVE('',#6963,#6928,#1586,.T.);
#9096=EDGE_CURVE('',#6967,#6961,#1587,.T.);
#9097=EDGE_CURVE('',#6966,#6967,#480,.T.);
#9098=EDGE_CURVE('',#6929,#6964,#1588,.T.);
#9099=EDGE_CURVE('',#6967,#6901,#1589,.T.);
#9100=EDGE_CURVE('',#6968,#6969,#4701,.T.);
#9101=EDGE_CURVE('',#6968,#6970,#4702,.T.);
#9102=EDGE_CURVE('',#6970,#6971,#4703,.T.);
#9103=EDGE_CURVE('',#6969,#6971,#4704,.T.);
#9104=EDGE_CURVE('',#6972,#6968,#4705,.T.);
#9105=EDGE_CURVE('',#6972,#6973,#4706,.T.);
#9106=EDGE_CURVE('',#6973,#6970,#4707,.T.);
#9107=EDGE_CURVE('',#6974,#6972,#4708,.T.);
#9108=EDGE_CURVE('',#6974,#6975,#4709,.T.);
#9109=EDGE_CURVE('',#6975,#6973,#4710,.T.);
#9110=EDGE_CURVE('',#6976,#6974,#4711,.T.);
#9111=EDGE_CURVE('',#6976,#6977,#4712,.T.);
#9112=EDGE_CURVE('',#6977,#6975,#4713,.T.);
#9113=EDGE_CURVE('',#6978,#6976,#4714,.T.);
#9114=EDGE_CURVE('',#6978,#6979,#4715,.T.);
#9115=EDGE_CURVE('',#6979,#6977,#4716,.T.);
#9116=EDGE_CURVE('',#6969,#6978,#4717,.T.);
#9117=EDGE_CURVE('',#6971,#6979,#4718,.T.);
#9118=EDGE_CURVE('',#6980,#6980,#481,.T.);
#9119=EDGE_CURVE('',#6980,#6981,#4719,.T.);
#9120=EDGE_CURVE('',#6981,#6981,#482,.T.);
#13145=ORIENTED_EDGE('',*,*,#8995,.F.);
#13146=ORIENTED_EDGE('',*,*,#8996,.T.);
#13147=ORIENTED_EDGE('',*,*,#8997,.T.);
#13148=ORIENTED_EDGE('',*,*,#8998,.T.);
#13149=ORIENTED_EDGE('',*,*,#8999,.F.);
#13150=ORIENTED_EDGE('',*,*,#9000,.T.);
#13151=ORIENTED_EDGE('',*,*,#8995,.T.);
#13152=ORIENTED_EDGE('',*,*,#9001,.T.);
#13153=ORIENTED_EDGE('',*,*,#9002,.F.);
#13154=ORIENTED_EDGE('',*,*,#9003,.T.);
#13155=ORIENTED_EDGE('',*,*,#8999,.T.);
#13156=ORIENTED_EDGE('',*,*,#9004,.T.);
#13157=ORIENTED_EDGE('',*,*,#9005,.F.);
#13158=ORIENTED_EDGE('',*,*,#9006,.T.);
#13159=ORIENTED_EDGE('',*,*,#9002,.T.);
#13160=ORIENTED_EDGE('',*,*,#9007,.T.);
#13161=ORIENTED_EDGE('',*,*,#9008,.F.);
#13162=ORIENTED_EDGE('',*,*,#9009,.T.);
#13163=ORIENTED_EDGE('',*,*,#9005,.T.);
#13164=ORIENTED_EDGE('',*,*,#9010,.T.);
#13165=ORIENTED_EDGE('',*,*,#9011,.F.);
#13166=ORIENTED_EDGE('',*,*,#9012,.T.);
#13167=ORIENTED_EDGE('',*,*,#9008,.T.);
#13168=ORIENTED_EDGE('',*,*,#9013,.T.);
#13169=ORIENTED_EDGE('',*,*,#9014,.F.);
#13170=ORIENTED_EDGE('',*,*,#9015,.T.);
#13171=ORIENTED_EDGE('',*,*,#9011,.T.);
#13172=ORIENTED_EDGE('',*,*,#9016,.T.);
#13173=ORIENTED_EDGE('',*,*,#9017,.F.);
#13174=ORIENTED_EDGE('',*,*,#9018,.T.);
#13175=ORIENTED_EDGE('',*,*,#9014,.T.);
#13176=ORIENTED_EDGE('',*,*,#9019,.T.);
#13177=ORIENTED_EDGE('',*,*,#9020,.F.);
#13178=ORIENTED_EDGE('',*,*,#9021,.T.);
#13179=ORIENTED_EDGE('',*,*,#9017,.T.);
#13180=ORIENTED_EDGE('',*,*,#9022,.T.);
#13181=ORIENTED_EDGE('',*,*,#9023,.F.);
#13182=ORIENTED_EDGE('',*,*,#9024,.T.);
#13183=ORIENTED_EDGE('',*,*,#9020,.T.);
#13184=ORIENTED_EDGE('',*,*,#9025,.T.);
#13185=ORIENTED_EDGE('',*,*,#9026,.F.);
#13186=ORIENTED_EDGE('',*,*,#9027,.T.);
#13187=ORIENTED_EDGE('',*,*,#9023,.T.);
#13188=ORIENTED_EDGE('',*,*,#9028,.T.);
#13189=ORIENTED_EDGE('',*,*,#9029,.F.);
#13190=ORIENTED_EDGE('',*,*,#9030,.T.);
#13191=ORIENTED_EDGE('',*,*,#9026,.T.);
#13192=ORIENTED_EDGE('',*,*,#9031,.T.);
#13193=ORIENTED_EDGE('',*,*,#9032,.F.);
#13194=ORIENTED_EDGE('',*,*,#9033,.T.);
#13195=ORIENTED_EDGE('',*,*,#9029,.T.);
#13196=ORIENTED_EDGE('',*,*,#9034,.T.);
#13197=ORIENTED_EDGE('',*,*,#9035,.F.);
#13198=ORIENTED_EDGE('',*,*,#9036,.T.);
#13199=ORIENTED_EDGE('',*,*,#9032,.T.);
#13200=ORIENTED_EDGE('',*,*,#9037,.T.);
#13201=ORIENTED_EDGE('',*,*,#9038,.F.);
#13202=ORIENTED_EDGE('',*,*,#9039,.T.);
#13203=ORIENTED_EDGE('',*,*,#9035,.T.);
#13204=ORIENTED_EDGE('',*,*,#9040,.T.);
#13205=ORIENTED_EDGE('',*,*,#9041,.F.);
#13206=ORIENTED_EDGE('',*,*,#9042,.T.);
#13207=ORIENTED_EDGE('',*,*,#9043,.T.);
#13208=ORIENTED_EDGE('',*,*,#9044,.F.);
#13209=ORIENTED_EDGE('',*,*,#9045,.F.);
#13210=ORIENTED_EDGE('',*,*,#9046,.T.);
#13211=ORIENTED_EDGE('',*,*,#9041,.T.);
#13212=ORIENTED_EDGE('',*,*,#9047,.F.);
#13213=ORIENTED_EDGE('',*,*,#9048,.F.);
#13214=ORIENTED_EDGE('',*,*,#9049,.T.);
#13215=ORIENTED_EDGE('',*,*,#9045,.T.);
#13216=ORIENTED_EDGE('',*,*,#9050,.F.);
#13217=ORIENTED_EDGE('',*,*,#9051,.F.);
#13218=ORIENTED_EDGE('',*,*,#9052,.T.);
#13219=ORIENTED_EDGE('',*,*,#9048,.T.);
#13220=ORIENTED_EDGE('',*,*,#9053,.F.);
#13221=ORIENTED_EDGE('',*,*,#9054,.F.);
#13222=ORIENTED_EDGE('',*,*,#9055,.T.);
#13223=ORIENTED_EDGE('',*,*,#9051,.T.);
#13224=ORIENTED_EDGE('',*,*,#9056,.F.);
#13225=ORIENTED_EDGE('',*,*,#9057,.F.);
#13226=ORIENTED_EDGE('',*,*,#9058,.T.);
#13227=ORIENTED_EDGE('',*,*,#9054,.T.);
#13228=ORIENTED_EDGE('',*,*,#9059,.F.);
#13229=ORIENTED_EDGE('',*,*,#9060,.F.);
#13230=ORIENTED_EDGE('',*,*,#9061,.T.);
#13231=ORIENTED_EDGE('',*,*,#9057,.T.);
#13232=ORIENTED_EDGE('',*,*,#9062,.F.);
#13233=ORIENTED_EDGE('',*,*,#9063,.F.);
#13234=ORIENTED_EDGE('',*,*,#9064,.T.);
#13235=ORIENTED_EDGE('',*,*,#9060,.T.);
#13236=ORIENTED_EDGE('',*,*,#9065,.F.);
#13237=ORIENTED_EDGE('',*,*,#9066,.F.);
#13238=ORIENTED_EDGE('',*,*,#9067,.T.);
#13239=ORIENTED_EDGE('',*,*,#9063,.T.);
#13240=ORIENTED_EDGE('',*,*,#9068,.F.);
#13241=ORIENTED_EDGE('',*,*,#9069,.F.);
#13242=ORIENTED_EDGE('',*,*,#9070,.T.);
#13243=ORIENTED_EDGE('',*,*,#9066,.T.);
#13244=ORIENTED_EDGE('',*,*,#9071,.F.);
#13245=ORIENTED_EDGE('',*,*,#9072,.F.);
#13246=ORIENTED_EDGE('',*,*,#9073,.T.);
#13247=ORIENTED_EDGE('',*,*,#9069,.T.);
#13248=ORIENTED_EDGE('',*,*,#9074,.F.);
#13249=ORIENTED_EDGE('',*,*,#9075,.F.);
#13250=ORIENTED_EDGE('',*,*,#9076,.T.);
#13251=ORIENTED_EDGE('',*,*,#9072,.T.);
#13252=ORIENTED_EDGE('',*,*,#9077,.F.);
#13253=ORIENTED_EDGE('',*,*,#9078,.F.);
#13254=ORIENTED_EDGE('',*,*,#9079,.T.);
#13255=ORIENTED_EDGE('',*,*,#9075,.T.);
#13256=ORIENTED_EDGE('',*,*,#9080,.F.);
#13257=ORIENTED_EDGE('',*,*,#9081,.F.);
#13258=ORIENTED_EDGE('',*,*,#9082,.T.);
#13259=ORIENTED_EDGE('',*,*,#9078,.T.);
#13260=ORIENTED_EDGE('',*,*,#9083,.F.);
#13261=ORIENTED_EDGE('',*,*,#9084,.F.);
#13262=ORIENTED_EDGE('',*,*,#9085,.T.);
#13263=ORIENTED_EDGE('',*,*,#9081,.T.);
#13264=ORIENTED_EDGE('',*,*,#9086,.F.);
#13265=ORIENTED_EDGE('',*,*,#9087,.F.);
#13266=ORIENTED_EDGE('',*,*,#9043,.F.);
#13267=ORIENTED_EDGE('',*,*,#9088,.F.);
#13268=ORIENTED_EDGE('',*,*,#9089,.F.);
#13269=ORIENTED_EDGE('',*,*,#9090,.F.);
#13270=ORIENTED_EDGE('',*,*,#9091,.T.);
#13271=ORIENTED_EDGE('',*,*,#9092,.F.);
#13272=ORIENTED_EDGE('',*,*,#9091,.F.);
#13273=ORIENTED_EDGE('',*,*,#9088,.T.);
#13274=ORIENTED_EDGE('',*,*,#9042,.F.);
#13275=ORIENTED_EDGE('',*,*,#9046,.F.);
#13276=ORIENTED_EDGE('',*,*,#9049,.F.);
#13277=ORIENTED_EDGE('',*,*,#9052,.F.);
#13278=ORIENTED_EDGE('',*,*,#9055,.F.);
#13279=ORIENTED_EDGE('',*,*,#9058,.F.);
#13280=ORIENTED_EDGE('',*,*,#9061,.F.);
#13281=ORIENTED_EDGE('',*,*,#9064,.F.);
#13282=ORIENTED_EDGE('',*,*,#9067,.F.);
#13283=ORIENTED_EDGE('',*,*,#9070,.F.);
#13284=ORIENTED_EDGE('',*,*,#9073,.F.);
#13285=ORIENTED_EDGE('',*,*,#9076,.F.);
#13286=ORIENTED_EDGE('',*,*,#9079,.F.);
#13287=ORIENTED_EDGE('',*,*,#9082,.F.);
#13288=ORIENTED_EDGE('',*,*,#9085,.F.);
#13289=ORIENTED_EDGE('',*,*,#9093,.F.);
#13290=ORIENTED_EDGE('',*,*,#9094,.F.);
#13291=ORIENTED_EDGE('',*,*,#8996,.F.);
#13292=ORIENTED_EDGE('',*,*,#9000,.F.);
#13293=ORIENTED_EDGE('',*,*,#9003,.F.);
#13294=ORIENTED_EDGE('',*,*,#9006,.F.);
#13295=ORIENTED_EDGE('',*,*,#9009,.F.);
#13296=ORIENTED_EDGE('',*,*,#9012,.F.);
#13297=ORIENTED_EDGE('',*,*,#9015,.F.);
#13298=ORIENTED_EDGE('',*,*,#9018,.F.);
#13299=ORIENTED_EDGE('',*,*,#9021,.F.);
#13300=ORIENTED_EDGE('',*,*,#9024,.F.);
#13301=ORIENTED_EDGE('',*,*,#9027,.F.);
#13302=ORIENTED_EDGE('',*,*,#9030,.F.);
#13303=ORIENTED_EDGE('',*,*,#9033,.F.);
#13304=ORIENTED_EDGE('',*,*,#9036,.F.);
#13305=ORIENTED_EDGE('',*,*,#9039,.F.);
#13306=ORIENTED_EDGE('',*,*,#9095,.F.);
#13307=ORIENTED_EDGE('',*,*,#9084,.T.);
#13308=ORIENTED_EDGE('',*,*,#9096,.F.);
#13309=ORIENTED_EDGE('',*,*,#9097,.F.);
#13310=ORIENTED_EDGE('',*,*,#9093,.T.);
#13311=ORIENTED_EDGE('',*,*,#9087,.T.);
#13312=ORIENTED_EDGE('',*,*,#9090,.T.);
#13313=ORIENTED_EDGE('',*,*,#9098,.F.);
#13314=ORIENTED_EDGE('',*,*,#9040,.F.);
#13315=ORIENTED_EDGE('',*,*,#9037,.F.);
#13316=ORIENTED_EDGE('',*,*,#9034,.F.);
#13317=ORIENTED_EDGE('',*,*,#9031,.F.);
#13318=ORIENTED_EDGE('',*,*,#9028,.F.);
#13319=ORIENTED_EDGE('',*,*,#9025,.F.);
#13320=ORIENTED_EDGE('',*,*,#9022,.F.);
#13321=ORIENTED_EDGE('',*,*,#9019,.F.);
#13322=ORIENTED_EDGE('',*,*,#9016,.F.);
#13323=ORIENTED_EDGE('',*,*,#9013,.F.);
#13324=ORIENTED_EDGE('',*,*,#9010,.F.);
#13325=ORIENTED_EDGE('',*,*,#9007,.F.);
#13326=ORIENTED_EDGE('',*,*,#9004,.F.);
#13327=ORIENTED_EDGE('',*,*,#9001,.F.);
#13328=ORIENTED_EDGE('',*,*,#8998,.F.);
#13329=ORIENTED_EDGE('',*,*,#9099,.F.);
#13330=ORIENTED_EDGE('',*,*,#9096,.T.);
#13331=ORIENTED_EDGE('',*,*,#9086,.T.);
#13332=ORIENTED_EDGE('',*,*,#9083,.T.);
#13333=ORIENTED_EDGE('',*,*,#9080,.T.);
#13334=ORIENTED_EDGE('',*,*,#9077,.T.);
#13335=ORIENTED_EDGE('',*,*,#9074,.T.);
#13336=ORIENTED_EDGE('',*,*,#9071,.T.);
#13337=ORIENTED_EDGE('',*,*,#9068,.T.);
#13338=ORIENTED_EDGE('',*,*,#9065,.T.);
#13339=ORIENTED_EDGE('',*,*,#9062,.T.);
#13340=ORIENTED_EDGE('',*,*,#9059,.T.);
#13341=ORIENTED_EDGE('',*,*,#9056,.T.);
#13342=ORIENTED_EDGE('',*,*,#9053,.T.);
#13343=ORIENTED_EDGE('',*,*,#9050,.T.);
#13344=ORIENTED_EDGE('',*,*,#9047,.T.);
#13345=ORIENTED_EDGE('',*,*,#9044,.T.);
#13346=ORIENTED_EDGE('',*,*,#9038,.T.);
#13347=ORIENTED_EDGE('',*,*,#9098,.T.);
#13348=ORIENTED_EDGE('',*,*,#9089,.T.);
#13349=ORIENTED_EDGE('',*,*,#9095,.T.);
#13350=ORIENTED_EDGE('',*,*,#9100,.F.);
#13351=ORIENTED_EDGE('',*,*,#9101,.T.);
#13352=ORIENTED_EDGE('',*,*,#9102,.T.);
#13353=ORIENTED_EDGE('',*,*,#9103,.F.);
#13354=ORIENTED_EDGE('',*,*,#9104,.F.);
#13355=ORIENTED_EDGE('',*,*,#9105,.T.);
#13356=ORIENTED_EDGE('',*,*,#9106,.T.);
#13357=ORIENTED_EDGE('',*,*,#9101,.F.);
#13358=ORIENTED_EDGE('',*,*,#9107,.F.);
#13359=ORIENTED_EDGE('',*,*,#9108,.T.);
#13360=ORIENTED_EDGE('',*,*,#9109,.T.);
#13361=ORIENTED_EDGE('',*,*,#9105,.F.);
#13362=ORIENTED_EDGE('',*,*,#9110,.F.);
#13363=ORIENTED_EDGE('',*,*,#9111,.T.);
#13364=ORIENTED_EDGE('',*,*,#9112,.T.);
#13365=ORIENTED_EDGE('',*,*,#9108,.F.);
#13366=ORIENTED_EDGE('',*,*,#9113,.F.);
#13367=ORIENTED_EDGE('',*,*,#9114,.T.);
#13368=ORIENTED_EDGE('',*,*,#9115,.T.);
#13369=ORIENTED_EDGE('',*,*,#9111,.F.);
#13370=ORIENTED_EDGE('',*,*,#9116,.F.);
#13371=ORIENTED_EDGE('',*,*,#9103,.T.);
#13372=ORIENTED_EDGE('',*,*,#9117,.T.);
#13373=ORIENTED_EDGE('',*,*,#9114,.F.);
#13374=ORIENTED_EDGE('',*,*,#9117,.F.);
#13375=ORIENTED_EDGE('',*,*,#9102,.F.);
#13376=ORIENTED_EDGE('',*,*,#9106,.F.);
#13377=ORIENTED_EDGE('',*,*,#9109,.F.);
#13378=ORIENTED_EDGE('',*,*,#9112,.F.);
#13379=ORIENTED_EDGE('',*,*,#9115,.F.);
#13380=ORIENTED_EDGE('',*,*,#9118,.T.);
#13381=ORIENTED_EDGE('',*,*,#9094,.T.);
#13382=ORIENTED_EDGE('',*,*,#9097,.T.);
#13383=ORIENTED_EDGE('',*,*,#9099,.T.);
#13384=ORIENTED_EDGE('',*,*,#8997,.F.);
#13385=ORIENTED_EDGE('',*,*,#9118,.F.);
#13386=ORIENTED_EDGE('',*,*,#9119,.T.);
#13387=ORIENTED_EDGE('',*,*,#9120,.T.);
#13388=ORIENTED_EDGE('',*,*,#9119,.F.);
#13389=ORIENTED_EDGE('',*,*,#9120,.F.);
#13390=ORIENTED_EDGE('',*,*,#9100,.T.);
#13391=ORIENTED_EDGE('',*,*,#9116,.T.);
#13392=ORIENTED_EDGE('',*,*,#9113,.T.);
#13393=ORIENTED_EDGE('',*,*,#9110,.T.);
#13394=ORIENTED_EDGE('',*,*,#9107,.T.);
#13395=ORIENTED_EDGE('',*,*,#9104,.T.);
#13396=ORIENTED_EDGE('',*,*,#9092,.T.);
#13537=PLANE('',#15473);
#13538=PLANE('',#15474);
#13539=PLANE('',#15475);
#13540=PLANE('',#15476);
#13541=PLANE('',#15477);
#13542=PLANE('',#15478);
#13543=PLANE('',#15479);
#13544=PLANE('',#15480);
#13545=PLANE('',#15484);
#13546=PLANE('',#15485);
#14259=ADVANCED_FACE('',(#3013),#2141,.T.);
#14260=ADVANCED_FACE('',(#3014),#2142,.T.);
#14261=ADVANCED_FACE('',(#3015),#2143,.T.);
#14262=ADVANCED_FACE('',(#3016),#2144,.T.);
#14263=ADVANCED_FACE('',(#3017),#2145,.T.);
#14264=ADVANCED_FACE('',(#3018),#2146,.T.);
#14265=ADVANCED_FACE('',(#3019),#2147,.T.);
#14266=ADVANCED_FACE('',(#3020),#2148,.T.);
#14267=ADVANCED_FACE('',(#3021),#2149,.T.);
#14268=ADVANCED_FACE('',(#3022),#2150,.T.);
#14269=ADVANCED_FACE('',(#3023),#2151,.T.);
#14270=ADVANCED_FACE('',(#3024),#2152,.T.);
#14271=ADVANCED_FACE('',(#3025),#2153,.T.);
#14272=ADVANCED_FACE('',(#3026),#2154,.T.);
#14273=ADVANCED_FACE('',(#3027),#2155,.T.);
#14274=ADVANCED_FACE('',(#3028),#2156,.T.);
#14275=ADVANCED_FACE('',(#3029),#2157,.T.);
#14276=ADVANCED_FACE('',(#3030),#2158,.T.);
#14277=ADVANCED_FACE('',(#3031),#2159,.T.);
#14278=ADVANCED_FACE('',(#3032),#2160,.T.);
#14279=ADVANCED_FACE('',(#3033),#2161,.T.);
#14280=ADVANCED_FACE('',(#3034),#2162,.T.);
#14281=ADVANCED_FACE('',(#3035),#2163,.T.);
#14282=ADVANCED_FACE('',(#3036),#2164,.T.);
#14283=ADVANCED_FACE('',(#3037),#2165,.T.);
#14284=ADVANCED_FACE('',(#3038),#2166,.T.);
#14285=ADVANCED_FACE('',(#3039),#2167,.T.);
#14286=ADVANCED_FACE('',(#3040),#2168,.T.);
#14287=ADVANCED_FACE('',(#3041),#2169,.T.);
#14288=ADVANCED_FACE('',(#3042),#2170,.T.);
#14289=ADVANCED_FACE('',(#3043),#256,.T.);
#14290=ADVANCED_FACE('',(#3044),#283,.F.);
#14291=ADVANCED_FACE('',(#3045),#2171,.T.);
#14292=ADVANCED_FACE('',(#3046),#284,.F.);
#14293=ADVANCED_FACE('',(#3047),#2172,.T.);
#14294=ADVANCED_FACE('',(#3048),#13537,.F.);
#14295=ADVANCED_FACE('',(#3049),#13538,.F.);
#14296=ADVANCED_FACE('',(#3050),#13539,.F.);
#14297=ADVANCED_FACE('',(#3051),#13540,.F.);
#14298=ADVANCED_FACE('',(#3052),#13541,.F.);
#14299=ADVANCED_FACE('',(#3053),#13542,.F.);
#14300=ADVANCED_FACE('',(#3054),#13543,.F.);
#14301=ADVANCED_FACE('',(#3055,#2299),#13544,.T.);
#14302=ADVANCED_FACE('',(#3056),#2173,.T.);
#14303=ADVANCED_FACE('',(#3057,#2300),#13545,.F.);
#14304=ADVANCED_FACE('',(#3058),#13546,.T.);
#14323=CLOSED_SHELL('',(#14259,#14260,#14261,#14262,#14263,#14264,#14265,
#14266,#14267,#14268,#14269,#14270,#14271,#14272,#14273,#14274,#14275,#14276,
#14277,#14278,#14279,#14280,#14281,#14282,#14283,#14284,#14285,#14286,#14287,
#14288,#14289,#14290,#14291,#14292,#14293,#14294,#14295,#14296,#14297,#14298,
#14299,#14300,#14301,#14302,#14303,#14304));
#15434=AXIS2_PLACEMENT_3D('',#61158,#18163,#18164);
#15435=AXIS2_PLACEMENT_3D('',#61159,#18165,#18166);
#15436=AXIS2_PLACEMENT_3D('',#61175,#18168,#18169);
#15437=AXIS2_PLACEMENT_3D('',#61183,#18170,#18171);
#15438=AXIS2_PLACEMENT_3D('',#61231,#18173,#18174);
#15439=AXIS2_PLACEMENT_3D('',#61279,#18176,#18177);
#15440=AXIS2_PLACEMENT_3D('',#61333,#18179,#18180);
#15441=AXIS2_PLACEMENT_3D('',#61381,#18182,#18183);
#15442=AXIS2_PLACEMENT_3D('',#61429,#18185,#18186);
#15443=AXIS2_PLACEMENT_3D('',#61483,#18188,#18189);
#15444=AXIS2_PLACEMENT_3D('',#61531,#18191,#18192);
#15445=AXIS2_PLACEMENT_3D('',#61579,#18194,#18195);
#15446=AXIS2_PLACEMENT_3D('',#61633,#18197,#18198);
#15447=AXIS2_PLACEMENT_3D('',#61681,#18200,#18201);
#15448=AXIS2_PLACEMENT_3D('',#61729,#18203,#18204);
#15449=AXIS2_PLACEMENT_3D('',#61783,#18206,#18207);
#15450=AXIS2_PLACEMENT_3D('',#61831,#18209,#18210);
#15451=AXIS2_PLACEMENT_3D('',#61879,#18212,#18213);
#15452=AXIS2_PLACEMENT_3D('',#61895,#18215,#18216);
#15453=AXIS2_PLACEMENT_3D('',#61904,#18217,#18218);
#15454=AXIS2_PLACEMENT_3D('',#61929,#18220,#18221);
#15455=AXIS2_PLACEMENT_3D('',#61953,#18223,#18224);
#15456=AXIS2_PLACEMENT_3D('',#61978,#18226,#18227);
#15457=AXIS2_PLACEMENT_3D('',#62003,#18229,#18230);
#15458=AXIS2_PLACEMENT_3D('',#62027,#18232,#18233);
#15459=AXIS2_PLACEMENT_3D('',#62052,#18235,#18236);
#15460=AXIS2_PLACEMENT_3D('',#62077,#18238,#18239);
#15461=AXIS2_PLACEMENT_3D('',#62101,#18241,#18242);
#15462=AXIS2_PLACEMENT_3D('',#62126,#18244,#18245);
#15463=AXIS2_PLACEMENT_3D('',#62151,#18247,#18248);
#15464=AXIS2_PLACEMENT_3D('',#62175,#18250,#18251);
#15465=AXIS2_PLACEMENT_3D('',#62200,#18253,#18254);
#15466=AXIS2_PLACEMENT_3D('',#62225,#18256,#18257);
#15467=AXIS2_PLACEMENT_3D('',#62249,#18259,#18260);
#15468=AXIS2_PLACEMENT_3D('',#62537,#18261,#18262);
#15469=AXIS2_PLACEMENT_3D('',#62571,#18264,#18265);
#15470=AXIS2_PLACEMENT_3D('',#63096,#18266,#18267);
#15471=AXIS2_PLACEMENT_3D('',#63107,#18268,#18269);
#15472=AXIS2_PLACEMENT_3D('',#63634,#18270,#18271);
#15473=AXIS2_PLACEMENT_3D('',#63635,#18272,#18273);
#15474=AXIS2_PLACEMENT_3D('',#63644,#18278,#18279);
#15475=AXIS2_PLACEMENT_3D('',#63650,#18283,#18284);
#15476=AXIS2_PLACEMENT_3D('',#63656,#18288,#18289);
#15477=AXIS2_PLACEMENT_3D('',#63662,#18293,#18294);
#15478=AXIS2_PLACEMENT_3D('',#63668,#18298,#18299);
#15479=AXIS2_PLACEMENT_3D('',#63671,#18302,#18303);
#15480=AXIS2_PLACEMENT_3D('',#63672,#18304,#18305);
#15481=AXIS2_PLACEMENT_3D('',#63674,#18306,#18307);
#15482=AXIS2_PLACEMENT_3D('',#63675,#18308,#18309);
#15483=AXIS2_PLACEMENT_3D('',#63678,#18311,#18312);
#15484=AXIS2_PLACEMENT_3D('',#63679,#18313,#18314);
#15485=AXIS2_PLACEMENT_3D('',#63680,#18315,#18316);
#18163=DIRECTION('axis',(0.,0.,1.));
#18164=DIRECTION('refdir',(1.,0.,0.));
#18165=DIRECTION('center_axis',(0.,0.,1.));
#18166=DIRECTION('ref_axis',(1.,0.,0.));
#18167=DIRECTION('',(0.,0.,-1.));
#18168=DIRECTION('center_axis',(0.,0.,-1.));
#18169=DIRECTION('ref_axis',(1.,0.,0.));
#18170=DIRECTION('center_axis',(0.,0.,1.));
#18171=DIRECTION('ref_axis',(1.,0.,0.));
#18172=DIRECTION('',(0.,0.,-1.));
#18173=DIRECTION('center_axis',(0.,0.,1.));
#18174=DIRECTION('ref_axis',(1.,0.,0.));
#18175=DIRECTION('',(0.,0.,-1.));
#18176=DIRECTION('center_axis',(0.,0.,1.));
#18177=DIRECTION('ref_axis',(1.,0.,0.));
#18178=DIRECTION('',(0.,0.,-1.));
#18179=DIRECTION('center_axis',(0.,0.,1.));
#18180=DIRECTION('ref_axis',(1.,0.,0.));
#18181=DIRECTION('',(0.,0.,-1.));
#18182=DIRECTION('center_axis',(0.,0.,1.));
#18183=DIRECTION('ref_axis',(1.,0.,0.));
#18184=DIRECTION('',(0.,0.,-1.));
#18185=DIRECTION('center_axis',(0.,0.,1.));
#18186=DIRECTION('ref_axis',(1.,0.,0.));
#18187=DIRECTION('',(0.,0.,-1.));
#18188=DIRECTION('center_axis',(0.,0.,1.));
#18189=DIRECTION('ref_axis',(1.,0.,0.));
#18190=DIRECTION('',(0.,0.,-1.));
#18191=DIRECTION('center_axis',(0.,0.,1.));
#18192=DIRECTION('ref_axis',(1.,0.,0.));
#18193=DIRECTION('',(0.,0.,-1.));
#18194=DIRECTION('center_axis',(0.,0.,1.));
#18195=DIRECTION('ref_axis',(1.,0.,0.));
#18196=DIRECTION('',(0.,0.,-1.));
#18197=DIRECTION('center_axis',(0.,0.,1.));
#18198=DIRECTION('ref_axis',(1.,0.,0.));
#18199=DIRECTION('',(0.,0.,-1.));
#18200=DIRECTION('center_axis',(0.,0.,1.));
#18201=DIRECTION('ref_axis',(1.,0.,0.));
#18202=DIRECTION('',(0.,0.,-1.));
#18203=DIRECTION('center_axis',(0.,0.,1.));
#18204=DIRECTION('ref_axis',(1.,0.,0.));
#18205=DIRECTION('',(0.,0.,-1.));
#18206=DIRECTION('center_axis',(0.,0.,1.));
#18207=DIRECTION('ref_axis',(1.,0.,0.));
#18208=DIRECTION('',(0.,0.,-1.));
#18209=DIRECTION('center_axis',(0.,0.,1.));
#18210=DIRECTION('ref_axis',(1.,0.,0.));
#18211=DIRECTION('',(0.,0.,-1.));
#18212=DIRECTION('center_axis',(0.,0.,1.));
#18213=DIRECTION('ref_axis',(0.997339946684471,-0.0728905394918792,0.));
#18214=DIRECTION('',(0.,0.,1.));
#18215=DIRECTION('center_axis',(0.,0.,-1.));
#18216=DIRECTION('ref_axis',(1.,1.10476514494527E-13,0.));
#18217=DIRECTION('center_axis',(0.,0.,1.));
#18218=DIRECTION('ref_axis',(1.,1.10476514494527E-13,0.));
#18219=DIRECTION('',(0.,0.,1.));
#18220=DIRECTION('center_axis',(0.,0.,1.));
#18221=DIRECTION('ref_axis',(1.,1.10476514494527E-13,0.));
#18222=DIRECTION('',(0.,0.,1.));
#18223=DIRECTION('center_axis',(0.,0.,1.));
#18224=DIRECTION('ref_axis',(1.,1.10476514494527E-13,0.));
#18225=DIRECTION('',(0.,0.,1.));
#18226=DIRECTION('center_axis',(0.,0.,1.));
#18227=DIRECTION('ref_axis',(1.,1.10476514494527E-13,0.));
#18228=DIRECTION('',(0.,0.,1.));
#18229=DIRECTION('center_axis',(0.,0.,1.));
#18230=DIRECTION('ref_axis',(1.,1.10476514494527E-13,0.));
#18231=DIRECTION('',(0.,0.,1.));
#18232=DIRECTION('center_axis',(0.,0.,1.));
#18233=DIRECTION('ref_axis',(1.,1.10476514494527E-13,0.));
#18234=DIRECTION('',(0.,0.,1.));
#18235=DIRECTION('center_axis',(0.,0.,1.));
#18236=DIRECTION('ref_axis',(1.,1.10476514494527E-13,0.));
#18237=DIRECTION('',(0.,0.,1.));
#18238=DIRECTION('center_axis',(0.,0.,1.));
#18239=DIRECTION('ref_axis',(1.,1.10476514494527E-13,0.));
#18240=DIRECTION('',(0.,0.,1.));
#18241=DIRECTION('center_axis',(0.,0.,1.));
#18242=DIRECTION('ref_axis',(1.,1.10476514494527E-13,0.));
#18243=DIRECTION('',(0.,0.,1.));
#18244=DIRECTION('center_axis',(0.,0.,1.));
#18245=DIRECTION('ref_axis',(1.,1.10476514494527E-13,0.));
#18246=DIRECTION('',(0.,0.,1.));
#18247=DIRECTION('center_axis',(0.,0.,1.));
#18248=DIRECTION('ref_axis',(1.,1.10476514494527E-13,0.));
#18249=DIRECTION('',(0.,0.,1.));
#18250=DIRECTION('center_axis',(0.,0.,1.));
#18251=DIRECTION('ref_axis',(1.,1.10476514494527E-13,0.));
#18252=DIRECTION('',(0.,0.,1.));
#18253=DIRECTION('center_axis',(0.,0.,1.));
#18254=DIRECTION('ref_axis',(1.,1.10476514494527E-13,0.));
#18255=DIRECTION('',(0.,0.,1.));
#18256=DIRECTION('center_axis',(0.,0.,1.));
#18257=DIRECTION('ref_axis',(1.,1.10476514494527E-13,0.));
#18258=DIRECTION('',(0.,0.,1.));
#18259=DIRECTION('center_axis',(0.,0.,-1.));
#18260=DIRECTION('ref_axis',(1.,0.,0.));
#18261=DIRECTION('center_axis',(0.,0.,-1.));
#18262=DIRECTION('ref_axis',(1.,0.,0.));
#18263=DIRECTION('',(0.707106781186547,8.65956056235493E-17,0.707106781186548));
#18264=DIRECTION('center_axis',(0.,0.,1.));
#18265=DIRECTION('ref_axis',(1.,0.,0.));
#18266=DIRECTION('center_axis',(0.,0.,1.));
#18267=DIRECTION('ref_axis',(1.,1.10476514494527E-13,0.));
#18268=DIRECTION('center_axis',(0.,0.,-1.));
#18269=DIRECTION('ref_axis',(1.,1.10476514494527E-13,0.));
#18270=DIRECTION('center_axis',(0.,0.,1.));
#18271=DIRECTION('ref_axis',(1.,0.,0.));
#18272=DIRECTION('center_axis',(-1.92296268638356E-16,-1.,0.));
#18273=DIRECTION('ref_axis',(1.,-1.92296268638356E-16,0.));
#18274=DIRECTION('',(1.,-1.92296268638356E-16,0.));
#18275=DIRECTION('',(0.,0.,1.));
#18276=DIRECTION('',(1.,-1.92296268638356E-16,0.));
#18277=DIRECTION('',(0.,0.,1.));
#18278=DIRECTION('center_axis',(-0.866025403784439,-0.5,0.));
#18279=DIRECTION('ref_axis',(0.5,-0.866025403784439,0.));
#18280=DIRECTION('',(0.5,-0.866025403784439,0.));
#18281=DIRECTION('',(0.,0.,1.));
#18282=DIRECTION('',(0.5,-0.866025403784439,0.));
#18283=DIRECTION('center_axis',(-0.866025403784439,0.5,0.));
#18284=DIRECTION('ref_axis',(-0.5,-0.866025403784438,0.));
#18285=DIRECTION('',(-0.5,-0.866025403784438,0.));
#18286=DIRECTION('',(0.,0.,1.));
#18287=DIRECTION('',(-0.5,-0.866025403784439,0.));
#18288=DIRECTION('center_axis',(1.92296268638356E-16,1.,0.));
#18289=DIRECTION('ref_axis',(-1.,1.92296268638356E-16,0.));
#18290=DIRECTION('',(-1.,1.92296268638356E-16,0.));
#18291=DIRECTION('',(0.,0.,1.));
#18292=DIRECTION('',(-1.,1.92296268638356E-16,0.));
#18293=DIRECTION('center_axis',(0.866025403784439,0.5,0.));
#18294=DIRECTION('ref_axis',(-0.5,0.866025403784439,0.));
#18295=DIRECTION('',(-0.5,0.866025403784439,0.));
#18296=DIRECTION('',(0.,0.,1.));
#18297=DIRECTION('',(-0.5,0.866025403784439,0.));
#18298=DIRECTION('center_axis',(0.866025403784439,-0.5,0.));
#18299=DIRECTION('ref_axis',(0.5,0.866025403784439,0.));
#18300=DIRECTION('',(0.5,0.866025403784439,0.));
#18301=DIRECTION('',(0.5,0.866025403784439,0.));
#18302=DIRECTION('center_axis',(0.,0.,1.));
#18303=DIRECTION('ref_axis',(1.,0.,0.));
#18304=DIRECTION('center_axis',(0.,0.,1.));
#18305=DIRECTION('ref_axis',(1.,0.,0.));
#18306=DIRECTION('center_axis',(0.,0.,1.));
#18307=DIRECTION('ref_axis',(1.,0.,0.));
#18308=DIRECTION('center_axis',(0.,0.,1.));
#18309=DIRECTION('ref_axis',(1.,0.,0.));
#18310=DIRECTION('',(0.,0.,-1.));
#18311=DIRECTION('center_axis',(0.,0.,1.));
#18312=DIRECTION('ref_axis',(1.,0.,0.));
#18313=DIRECTION('center_axis',(0.,0.,1.));
#18314=DIRECTION('ref_axis',(1.,0.,0.));
#18315=DIRECTION('center_axis',(0.,0.,1.));
#18316=DIRECTION('ref_axis',(1.,0.,0.));
#61158=CARTESIAN_POINT('',(0.,0.,0.));
#61159=CARTESIAN_POINT('Origin',(0.,0.,0.));
#61160=CARTESIAN_POINT('',(-2.94490570994055,0.00214417779480537,0.322176117089595));
#61161=CARTESIAN_POINT('',(-2.94453111094736,0.00313617179185542,0.177823882910391));
#61162=CARTESIAN_POINT('',(-2.942,-3.60291088309151E-16,0.));
#61163=CARTESIAN_POINT('',(1.28892185405323,2.64462557919718,0.));
#61164=CARTESIAN_POINT('Ctrl Pts',(-2.94490570994055,0.00214417779480537,
0.322176117089595));
#61165=CARTESIAN_POINT('Ctrl Pts',(-2.94584715833611,0.124808428590093,
0.315520895872749));
#61166=CARTESIAN_POINT('Ctrl Pts',(-2.93884007386573,0.247358426874668,
0.308865674655903));
#61167=CARTESIAN_POINT('Ctrl Pts',(-2.92351947045398,0.368852411761562,
0.302210453439057));
#61168=CARTESIAN_POINT('Ctrl Pts',(-2.80238513102988,1.32946037267173,0.249590083068687));
#61169=CARTESIAN_POINT('Ctrl Pts',(-2.16153286152783,2.22405187279705,0.196969712698316));
#61170=CARTESIAN_POINT('Ctrl Pts',(-1.29099252632988,2.64857098947325,0.144349342327946));
#61171=CARTESIAN_POINT('Ctrl Pts',(-0.494964144347145,3.03675434170317,
0.0962328948852971));
#61172=CARTESIAN_POINT('Ctrl Pts',(0.493115753268411,3.03189109212113,0.0481164474426485));
#61173=CARTESIAN_POINT('Ctrl Pts',(1.29200104020318,2.64812001020929,-1.63834222883338E-16));
#61174=CARTESIAN_POINT('',(-1.28892185405328,2.64462557919715,0.));
#61175=CARTESIAN_POINT('Origin',(0.,0.,0.));
#61176=CARTESIAN_POINT('Ctrl Pts',(-1.28892185405328,2.64462557919715,2.08166817117217E-15));
#61177=CARTESIAN_POINT('Ctrl Pts',(-2.16403831185616,2.21811653527939,0.0526649636666859));
#61178=CARTESIAN_POINT('Ctrl Pts',(-2.80357657272064,1.32706756586464,0.10532992733337));
#61179=CARTESIAN_POINT('Ctrl Pts',(-2.92355402589586,0.366959843828546,
0.157994891000053));
#61180=CARTESIAN_POINT('Ctrl Pts',(-2.93861167702227,0.246462477535227,
0.164604554970166));
#61181=CARTESIAN_POINT('Ctrl Pts',(-2.94548559297357,0.124877349165528,
0.171214218940278));
#61182=CARTESIAN_POINT('Ctrl Pts',(-2.94453111094736,0.00313617179185542,
0.177823882910391));
#61183=CARTESIAN_POINT('Origin',(0.,0.,0.));
#61184=CARTESIAN_POINT('',(-2.93741501075088,0.000605053430647595,1.3221761170896));
#61185=CARTESIAN_POINT('',(-2.93743260967528,0.000720687897601403,1.17782388291039));
#61186=CARTESIAN_POINT('',(-2.942,-3.60291088309151E-16,0.));
#61187=CARTESIAN_POINT('Ctrl Pts',(-2.93741501075088,0.000605053430647595,
1.3221761170896));
#61188=CARTESIAN_POINT('Ctrl Pts',(-2.9382479568139,0.450815163107398,1.29790978476164));
#61189=CARTESIAN_POINT('Ctrl Pts',(-2.84099804532476,0.900683451883265,
1.27364345243368));
#61190=CARTESIAN_POINT('Ctrl Pts',(-2.64378204823906,1.30134356458571,1.24937712010572));
#61191=CARTESIAN_POINT('Ctrl Pts',(-2.21612867774369,2.17015567999336,1.19675674973535));
#61192=CARTESIAN_POINT('Ctrl Pts',(-1.31841648749453,2.80758195059898,1.14413637936498));
#61193=CARTESIAN_POINT('Ctrl Pts',(-0.357192829781819,2.92497002089294,
1.09151600899461));
#61194=CARTESIAN_POINT('Ctrl Pts',(0.604030827930888,3.04235809118689,1.03889563862424));
#61195=CARTESIAN_POINT('Ctrl Pts',(1.62876595310715,2.63970796116917,0.986275268253872));
#61196=CARTESIAN_POINT('Ctrl Pts',(2.25292793158662,1.89932766827126,0.933654897883501));
#61197=CARTESIAN_POINT('Ctrl Pts',(2.8770899100661,1.15894737537334,0.881034527513131));
#61198=CARTESIAN_POINT('Ctrl Pts',(3.1006787418488,0.0808369195952267,0.828414157142761));
#61199=CARTESIAN_POINT('Ctrl Pts',(2.82245137682484,-0.846673957408537,
0.775793786772391));
#61200=CARTESIAN_POINT('Ctrl Pts',(2.54422401180089,-1.7741848344123,0.72317341640202));
#61201=CARTESIAN_POINT('Ctrl Pts',(1.76418044997028,-2.55109613264171,0.67055304603165));
#61202=CARTESIAN_POINT('Ctrl Pts',(0.835554749603298,-2.82571794203434,
0.617932675661279));
#61203=CARTESIAN_POINT('Ctrl Pts',(-0.0930709507636752,-3.10033975142697,
0.565312305290909));
#61204=CARTESIAN_POINT('Ctrl Pts',(-1.17027878966702,-2.87267207198282,
0.512691934920538));
#61205=CARTESIAN_POINT('Ctrl Pts',(-1.90817450444562,-2.24552602141323,
0.460071564550168));
#61206=CARTESIAN_POINT('Ctrl Pts',(-2.55274401908064,-1.69769898118953,
0.414106415396644));
#61207=CARTESIAN_POINT('Ctrl Pts',(-2.93840347440061,-0.845052391620324,
0.368141266243119));
#61208=CARTESIAN_POINT('Ctrl Pts',(-2.94490570994055,0.00214417779480537,
0.322176117089595));
#61209=CARTESIAN_POINT('Ctrl Pts',(-2.94453111094736,0.00313617179185542,
0.177823882910391));
#61210=CARTESIAN_POINT('Ctrl Pts',(-2.93788040132423,-0.845140901703999,
0.223879182606963));
#61211=CARTESIAN_POINT('Ctrl Pts',(-2.55115114237882,-1.7009943502416,0.269934482303535));
#61212=CARTESIAN_POINT('Ctrl Pts',(-1.90455354763271,-2.24922658650796,
0.315989782000107));
#61213=CARTESIAN_POINT('Ctrl Pts',(-1.16515897070839,-2.87613882015091,
0.368654745666792));
#61214=CARTESIAN_POINT('Ctrl Pts',(-0.0859531713737992,-3.10079681277935,
0.421319709333476));
#61215=CARTESIAN_POINT('Ctrl Pts',(0.842833952810694,-2.82335342322726,
0.473984673000161));
#61216=CARTESIAN_POINT('Ctrl Pts',(1.77162107699519,-2.54591003367518,0.526649636666845));
#61217=CARTESIAN_POINT('Ctrl Pts',(2.54998952602959,-1.76636526194256,0.57931460033353));
#61218=CARTESIAN_POINT('Ctrl Pts',(2.82526196809064,-0.837265996441287,
0.631979564000215));
#61219=CARTESIAN_POINT('Ctrl Pts',(3.1005344101517,0.0918332690599885,0.684644527666899));
#61220=CARTESIAN_POINT('Ctrl Pts',(2.87271084523941,1.17048702832993,0.737309491333584));
#61221=CARTESIAN_POINT('Ctrl Pts',(2.2449320231631,1.90890163868963,0.789974455000268));
#61222=CARTESIAN_POINT('Ctrl Pts',(1.61715320108678,2.64731624904933,0.842639418666953));
#61223=CARTESIAN_POINT('Ctrl Pts',(0.589419121846451,3.0454917104988,0.895304382333637));
#61224=CARTESIAN_POINT('Ctrl Pts',(-0.37200976733393,2.9231058378395,0.947969346000322));
#61225=CARTESIAN_POINT('Ctrl Pts',(-1.33343865651431,2.8007199651802,1.00063430966701));
#61226=CARTESIAN_POINT('Ctrl Pts',(-2.22856235563474,2.15777275841214,1.05329927333369));
#61227=CARTESIAN_POINT('Ctrl Pts',(-2.6514251854394,1.28574400496261,1.10596423700038));
#61228=CARTESIAN_POINT('Ctrl Pts',(-2.8437527539192,0.889125626674557,1.12991745230371));
#61229=CARTESIAN_POINT('Ctrl Pts',(-2.93838674329414,0.445118617110292,
1.15387066760705));
#61230=CARTESIAN_POINT('Ctrl Pts',(-2.93743260967528,0.000720687897601403,
1.17782388291039));
#61231=CARTESIAN_POINT('Origin',(0.,0.,0.));
#61232=CARTESIAN_POINT('',(-2.94283216929169,-0.00254059509496668,2.3221761170896));
#61233=CARTESIAN_POINT('',(-2.94249560619114,-0.00258942729680482,2.17782388291039));
#61234=CARTESIAN_POINT('',(-2.942,-3.60291088309151E-16,0.));
#61235=CARTESIAN_POINT('Ctrl Pts',(-2.94283216929169,-0.00254059509496668,
2.3221761170896));
#61236=CARTESIAN_POINT('Ctrl Pts',(-2.93583836831966,0.770783310741536,
2.28029867365053));
#61237=CARTESIAN_POINT('Ctrl Pts',(-2.62244249954969,1.54912568223824,2.23842123021146));
#61238=CARTESIAN_POINT('Ctrl Pts',(-2.07534059520784,2.09189740289201,2.19654378677239));
#61239=CARTESIAN_POINT('Ctrl Pts',(-1.38788924974329,2.77390773164861,2.14392341640202));
#61240=CARTESIAN_POINT('Ctrl Pts',(-0.331445515483537,3.08398167899393,
2.09130304603165));
#61241=CARTESIAN_POINT('Ctrl Pts',(0.615553755286461,2.88169496582278,2.03868267566128));
#61242=CARTESIAN_POINT('Ctrl Pts',(1.56255302605646,2.67940825265162,1.98606230529091));
#61243=CARTESIAN_POINT('Ctrl Pts',(2.40010783333669,1.96476087896396,1.93344193492054));
#61244=CARTESIAN_POINT('Ctrl Pts',(2.74891040156469,1.06139789331815,1.88082156455017));
#61245=CARTESIAN_POINT('Ctrl Pts',(3.09771296979268,0.158034907672333,1.8282011941798));
#61246=CARTESIAN_POINT('Ctrl Pts',(2.95776329896845,-0.934043689931643,
1.77558082380943));
#61247=CARTESIAN_POINT('Ctrl Pts',(2.39244139669332,-1.72026117030417,1.72296045343906));
#61248=CARTESIAN_POINT('Ctrl Pts',(1.82711949441818,-2.50647865067671,1.67034008306869));
#61249=CARTESIAN_POINT('Ctrl Pts',(0.836425360692154,-2.9868350138178,1.61771971269832));
#61250=CARTESIAN_POINT('Ctrl Pts',(-0.130980997368149,-2.9437920444354,
1.56509934232795));
#61251=CARTESIAN_POINT('Ctrl Pts',(-1.09838735542844,-2.90074907505299,
1.51247897195758));
#61252=CARTESIAN_POINT('Ctrl Pts',(-2.04250593782301,-2.33430677314711,
1.45985860158721));
#61253=CARTESIAN_POINT('Ctrl Pts',(-2.5357679536495,-1.50098664208934,1.40723823121684));
#61254=CARTESIAN_POINT('Ctrl Pts',(-2.80155798635321,-1.05195919262036,
1.37888419317442));
#61255=CARTESIAN_POINT('Ctrl Pts',(-2.93644175348072,-0.525443729069001,
1.35053015513201));
#61256=CARTESIAN_POINT('Ctrl Pts',(-2.93741501075088,0.000605053430647595,
1.3221761170896));
#61257=CARTESIAN_POINT('Ctrl Pts',(-2.93743260967528,0.000720687897601403,
1.17782388291039));
#61258=CARTESIAN_POINT('Ctrl Pts',(-2.93628892837727,-0.53196109845813,
1.20653563127374));
#61259=CARTESIAN_POINT('Ctrl Pts',(-2.79780571115684,-1.06520455211536,
1.23524737963708));
#61260=CARTESIAN_POINT('Ctrl Pts',(-2.52560900690579,-1.51806949138664,
1.26395912800043));
#61261=CARTESIAN_POINT('Ctrl Pts',(-2.02632803807862,-2.34874393415536,
1.31662409166711));
#61262=CARTESIAN_POINT('Ctrl Pts',(-1.07716413993538,-2.9089825195618,1.3692890553338));
#61263=CARTESIAN_POINT('Ctrl Pts',(-0.108652539320438,-2.94471329972367,
1.42195401900048));
#61264=CARTESIAN_POINT('Ctrl Pts',(0.85985906129451,-2.98044407988555,1.47461898266717));
#61265=CARTESIAN_POINT('Ctrl Pts',(1.84771836438116,-2.49166705480286,1.52728394633385));
#61266=CARTESIAN_POINT('Ctrl Pts',(2.40686102399513,-1.70005997098112,1.57994891000054));
#61267=CARTESIAN_POINT('Ctrl Pts',(2.9660036836091,-0.908452887159384,1.63261387366722));
#61268=CARTESIAN_POINT('Ctrl Pts',(3.09642969975039,0.185984255401396,1.68527883733391));
#61269=CARTESIAN_POINT('Ctrl Pts',(2.73897659148843,1.08682694396802,1.73794380100059));
#61270=CARTESIAN_POINT('Ctrl Pts',(2.38152348322647,1.98766963253464,1.79060876466727));
#61271=CARTESIAN_POINT('Ctrl Pts',(1.53619125056127,2.69491786710711,1.84327372833396));
#61272=CARTESIAN_POINT('Ctrl Pts',(0.586406744725485,2.88778465426983,1.89593869200064));
#61273=CARTESIAN_POINT('Ctrl Pts',(-0.363377761110303,3.08065144143255,
1.94860365566733));
#61274=CARTESIAN_POINT('Ctrl Pts',(-1.41761454011667,2.75913678118554,2.00126861933401));
#61275=CARTESIAN_POINT('Ctrl Pts',(-2.09812527093809,2.0690698668059,2.0539335830007));
#61276=CARTESIAN_POINT('Ctrl Pts',(-2.63174175688638,1.52795998382732,2.09523034963726));
#61277=CARTESIAN_POINT('Ctrl Pts',(-2.93556254699721,0.76023565397735,2.13652711627383));
#61278=CARTESIAN_POINT('Ctrl Pts',(-2.94249560619114,-0.00258942729680482,
2.17782388291039));
#61279=CARTESIAN_POINT('Origin',(0.,0.,0.));
#61280=CARTESIAN_POINT('',(-2.94484294150901,0.00199174253909633,3.3221761170896));
#61281=CARTESIAN_POINT('',(-2.94526037616607,0.00180040430511289,3.17782388291039));
#61282=CARTESIAN_POINT('',(-2.942,-3.60291088309151E-16,0.));
#61283=CARTESIAN_POINT('Ctrl Pts',(-2.94484294150901,0.00199174253909633,
3.3221761170896));
#61284=CARTESIAN_POINT('Ctrl Pts',(-2.94583002736539,0.128597483532049,
3.31530793290979));
#61285=CARTESIAN_POINT('Ctrl Pts',(-2.93836342958051,0.255086036799256,
3.30843974872998));
#61286=CARTESIAN_POINT('Ctrl Pts',(-2.92204585589404,0.380422278131109,
3.30157156455017));
#61287=CARTESIAN_POINT('Ctrl Pts',(-2.79702929424561,1.34068182665933,3.2489511941798));
#61288=CARTESIAN_POINT('Ctrl Pts',(-2.15247739366928,2.23330287085301,3.19633082380943));
#61289=CARTESIAN_POINT('Ctrl Pts',(-1.28029158434589,2.65403966800756,3.14371045343906));
#61290=CARTESIAN_POINT('Ctrl Pts',(-0.4081057750225,3.0747764651621,3.09109008306869));
#61291=CARTESIAN_POINT('Ctrl Pts',(0.69171394304795,3.0236290152775,3.03846971269832));
#61292=CARTESIAN_POINT('Ctrl Pts',(1.5210867384019,2.5237607280468,2.98584934232795));
#61293=CARTESIAN_POINT('Ctrl Pts',(2.35045953375586,2.0238924408161,2.93322897195758));
#61294=CARTESIAN_POINT('Ctrl Pts',(2.90938540639331,1.07530331623929,2.8806086015872));
#61295=CARTESIAN_POINT('Ctrl Pts',(2.94474080948057,0.107585617606989,2.82798823121683));
#61296=CARTESIAN_POINT('Ctrl Pts',(2.98009621256783,-0.860132081025304,
2.77536786084646));
#61297=CARTESIAN_POINT('Ctrl Pts',(2.49188114610491,-1.84697835371309,2.7227474904761));
#61298=CARTESIAN_POINT('Ctrl Pts',(1.70119600494326,-2.40603518007504,2.67012712010573));
#61299=CARTESIAN_POINT('Ctrl Pts',(0.91051086378161,-2.965092006437,2.61750674973535));
#61300=CARTESIAN_POINT('Ctrl Pts',(-0.182644352078765,-3.09635938647313,
2.56488637936498));
#61301=CARTESIAN_POINT('Ctrl Pts',(-1.08320700768761,-2.74038967310636,
2.51226600899461));
#61302=CARTESIAN_POINT('Ctrl Pts',(-1.98376966329644,-2.3844199597396,2.45964563862424));
#61303=CARTESIAN_POINT('Ctrl Pts',(-2.69173975865374,-1.54121315296996,
2.40702526825387));
#61304=CARTESIAN_POINT('Ctrl Pts',(-2.88649532799773,-0.59263639450121,
2.3544048978835));
#61305=CARTESIAN_POINT('Ctrl Pts',(-2.92625644781122,-0.398975826678611,
2.3436619709522));
#61306=CARTESIAN_POINT('Ctrl Pts',(-2.94462630681883,-0.200923340849699,
2.3329190440209));
#61307=CARTESIAN_POINT('Ctrl Pts',(-2.94283216929169,-0.00254059509496668,
2.3221761170896));
#61308=CARTESIAN_POINT('Ctrl Pts',(-2.94249560619114,-0.00258942729680482,
2.17782388291039));
#61309=CARTESIAN_POINT('Ctrl Pts',(-2.94440414260591,-0.212580342560449,
2.18919207994051));
#61310=CARTESIAN_POINT('Ctrl Pts',(-2.92381470891138,-0.422199995772688,
2.20056027697063));
#61311=CARTESIAN_POINT('Ctrl Pts',(-2.87932772554241,-0.626618874207943,
2.21192847400075));
#61312=CARTESIAN_POINT('Ctrl Pts',(-2.67323476668884,-1.57362153232989,
2.26459343766743));
#61313=CARTESIAN_POINT('Ctrl Pts',(-1.95426416634525,-2.40900768006153,
2.31725840133412));
#61314=CARTESIAN_POINT('Ctrl Pts',(-1.04852602468143,-2.75386472764491,
2.3699233650008));
#61315=CARTESIAN_POINT('Ctrl Pts',(-0.142787883017607,-3.09872177522829,
2.42258832866749));
#61316=CARTESIAN_POINT('Ctrl Pts',(0.949717799966449,-2.95304972266342,
2.47525329233417));
#61317=CARTESIAN_POINT('Ctrl Pts',(1.7334537997702,-2.38292188563198,2.52791825600086));
#61318=CARTESIAN_POINT('Ctrl Pts',(2.51718979957395,-1.81279404860055,2.58058321966754));
#61319=CARTESIAN_POINT('Ctrl Pts',(2.99215611619739,-0.818210427102559,
2.63324818333423));
#61320=CARTESIAN_POINT('Ctrl Pts',(2.94291803037279,0.149706737509724,2.68591314700091));
#61321=CARTESIAN_POINT('Ctrl Pts',(2.89367994454819,1.11762390212201,2.7385781106676));
#61322=CARTESIAN_POINT('Ctrl Pts',(2.32023745627556,2.05887460984858,2.79124307433428));
#61323=CARTESIAN_POINT('Ctrl Pts',(1.4826919461771,2.54652764310569,2.84390803800096));
#61324=CARTESIAN_POINT('Ctrl Pts',(0.645146436078633,3.03418067636279,2.89657300166765));
#61325=CARTESIAN_POINT('Ctrl Pts',(-0.456502095845658,3.06823603515044,
2.94923796533433));
#61326=CARTESIAN_POINT('Ctrl Pts',(-1.32256928803916,2.63324686948073,3.00190292900102));
#61327=CARTESIAN_POINT('Ctrl Pts',(-2.18863648023266,2.19825770381101,3.0545678926677));
#61328=CARTESIAN_POINT('Ctrl Pts',(-2.81912233269536,1.29422401368392,3.10723285633439));
#61329=CARTESIAN_POINT('Ctrl Pts',(-2.92805183726137,0.331196319314338,
3.15989782000107));
#61330=CARTESIAN_POINT('Ctrl Pts',(-2.94041095304778,0.221931425219236,
3.16587317430418));
#61331=CARTESIAN_POINT('Ctrl Pts',(-2.94605601250203,0.111907094355046,
3.17184852860728));
#61332=CARTESIAN_POINT('Ctrl Pts',(-2.94526037616607,0.00180040430511289,
3.17782388291039));
#61333=CARTESIAN_POINT('Origin',(0.,0.,0.));
#61334=CARTESIAN_POINT('',(-2.93739242931988,0.000540407572186541,4.3221761170896));
#61335=CARTESIAN_POINT('',(-2.93753500859377,0.000882026442511373,4.17782388291039));
#61336=CARTESIAN_POINT('',(-2.942,-3.60291088309151E-16,0.));
#61337=CARTESIAN_POINT('Ctrl Pts',(-2.93739242931988,0.000540407572186541,
4.3221761170896));
#61338=CARTESIAN_POINT('Ctrl Pts',(-2.93814630501522,0.454709257120266,
4.29769682179868));
#61339=CARTESIAN_POINT('Ctrl Pts',(-2.83910536028106,0.908566671316128,
4.27321752650776));
#61340=CARTESIAN_POINT('Ctrl Pts',(-2.6385374625564,1.31194251096478,4.24873823121684));
#61341=CARTESIAN_POINT('Ctrl Pts',(-2.20739935432037,2.17903389691023,4.19611786084646));
#61342=CARTESIAN_POINT('Ctrl Pts',(-1.30713327152341,2.8128638865229,4.14349749047609));
#61343=CARTESIAN_POINT('Ctrl Pts',(-0.345447198709921,2.92638673563265,
4.09087712010572));
#61344=CARTESIAN_POINT('Ctrl Pts',(0.616238874103564,3.0399095847424,4.03825674973536));
#61345=CARTESIAN_POINT('Ctrl Pts',(1.63934493693357,2.63312529334921,3.98563637936499));
#61346=CARTESIAN_POINT('Ctrl Pts',(2.26053185174972,1.89025628960273,3.93301600899462));
#61347=CARTESIAN_POINT('Ctrl Pts',(2.88171876656588,1.14738728585625,3.88039563862425));
#61348=CARTESIAN_POINT('Ctrl Pts',(3.10098653336818,0.0684335697564567,
3.82777526825387));
#61349=CARTESIAN_POINT('Ctrl Pts',(2.8190342665149,-0.857973716122647,3.7751548978835));
#61350=CARTESIAN_POINT('Ctrl Pts',(2.53708199966161,-1.78438100200175,3.72253452751313));
#61351=CARTESIAN_POINT('Ctrl Pts',(1.75390969915275,-2.55824185766015,3.66991415714276));
#61352=CARTESIAN_POINT('Ctrl Pts',(0.824196505293748,-2.82909406262337,
3.61729378677239));
#61353=CARTESIAN_POINT('Ctrl Pts',(-0.105516688565254,-3.09994626758658,
3.56467341640202));
#61354=CARTESIAN_POINT('Ctrl Pts',(-1.18177077577439,-2.86778982185459,
3.51205304603165));
#61355=CARTESIAN_POINT('Ctrl Pts',(-1.91715720801869,-2.23776257255722,
3.45943267566128));
#61356=CARTESIAN_POINT('Ctrl Pts',(-2.55655857926025,-1.68996855643583,
3.41368048947072));
#61357=CARTESIAN_POINT('Ctrl Pts',(-2.93826750108625,-0.841388295482023,
3.36792830328016));
#61358=CARTESIAN_POINT('Ctrl Pts',(-2.94484294150901,0.00199174253909633,
3.3221761170896));
#61359=CARTESIAN_POINT('Ctrl Pts',(-2.94526037616607,0.00180040430511289,
3.17782388291039));
#61360=CARTESIAN_POINT('Ctrl Pts',(-2.93904351473207,-0.858539934689441,
3.22451349227397));
#61361=CARTESIAN_POINT('Ctrl Pts',(-2.53959728591596,-1.72390862024193,
3.27120310163755));
#61362=CARTESIAN_POINT('Ctrl Pts',(-1.87733008879233,-2.27130145042432,
3.31789271100113));
#61363=CARTESIAN_POINT('Ctrl Pts',(-1.13030567908798,-2.88874982718133,
3.37055767466781));
#61364=CARTESIAN_POINT('Ctrl Pts',(-0.0488837030099704,-3.10162488208327,
3.4232226383345));
#61365=CARTESIAN_POINT('Ctrl Pts',(0.876425794829888,-2.81337100100799,
3.47588760200118));
#61366=CARTESIAN_POINT('Ctrl Pts',(1.80173529266975,-2.5251171199327,3.52855256566786));
#61367=CARTESIAN_POINT('Ctrl Pts',(2.57093231227146,-1.73573430288019,3.58121752933455));
#61368=CARTESIAN_POINT('Ctrl Pts',(2.83512541526138,-0.803269840348294,
3.63388249300123));
#61369=CARTESIAN_POINT('Ctrl Pts',(3.0993185182513,0.129194622183599,3.68654745666792));
#61370=CARTESIAN_POINT('Ctrl Pts',(2.85850770462944,1.20474073019488,3.7392124203346));
#61371=CARTESIAN_POINT('Ctrl Pts',(2.22191964750238,1.93552360728328,3.79187738400129));
#61372=CARTESIAN_POINT('Ctrl Pts',(1.58533159037532,2.66630648437168,3.84454234766797));
#61373=CARTESIAN_POINT('Ctrl Pts',(0.552966289743035,3.05232613053722,3.89720731133465));
#61374=CARTESIAN_POINT('Ctrl Pts',(-0.406917273431679,2.91849222887777,
3.94987227500134));
#61375=CARTESIAN_POINT('Ctrl Pts',(-1.36680083660641,2.78465832721833,4.00253723866802));
#61376=CARTESIAN_POINT('Ctrl Pts',(-2.25420266232356,2.13097087773392,4.05520220233471));
#61377=CARTESIAN_POINT('Ctrl Pts',(-2.666616123304,1.25392862924115,4.10786716600139));
#61378=CARTESIAN_POINT('Ctrl Pts',(-2.84922387445754,0.865593310885713,
4.13118607163773));
#61379=CARTESIAN_POINT('Ctrl Pts',(-2.9387088904313,0.433468688742346,4.15450497727406));
#61380=CARTESIAN_POINT('Ctrl Pts',(-2.93753500859377,0.000882026442511374,
4.17782388291039));
#61381=CARTESIAN_POINT('Origin',(0.,0.,0.));
#61382=CARTESIAN_POINT('',(-2.94294893056736,-0.00252441656932667,5.3221761170896));
#61383=CARTESIAN_POINT('',(-2.94214529852914,-0.00261326515612426,5.1778238829104));
#61384=CARTESIAN_POINT('',(-2.942,-3.60291088309151E-16,0.));
#61385=CARTESIAN_POINT('Ctrl Pts',(-2.94294893056736,-0.00252441656932667,
5.3221761170896));
#61386=CARTESIAN_POINT('Ctrl Pts',(-2.93593381851913,0.774652637504292,
5.28008571068756));
#61387=CARTESIAN_POINT('Ctrl Pts',(-2.61899610205614,1.55689120032164,5.23799530428553));
#61388=CARTESIAN_POINT('Ctrl Pts',(-2.06692649506365,2.10021140779169,5.1959048978835));
#61389=CARTESIAN_POINT('Ctrl Pts',(-1.37674291943613,2.77945670358908,5.14328452751313));
#61390=CARTESIAN_POINT('Ctrl Pts',(-0.31906293568821,3.08528758407071,5.09066415714276));
#61391=CARTESIAN_POINT('Ctrl Pts',(0.627116654359043,2.8792008952563,5.03804378677239));
#61392=CARTESIAN_POINT('Ctrl Pts',(1.5732962444063,2.67311420644189,4.98542341640202));
#61393=CARTESIAN_POINT('Ctrl Pts',(2.4079754407529,1.95510994833143,4.93280304603165));
#61394=CARTESIAN_POINT('Ctrl Pts',(2.75314891878373,1.05035428518759,4.88018267566128));
#61395=CARTESIAN_POINT('Ctrl Pts',(3.09832239681456,0.145598622043775,4.82756230529091));
#61396=CARTESIAN_POINT('Ctrl Pts',(2.95399015652965,-0.945908446133409,
4.77494193492054));
#61397=CARTESIAN_POINT('Ctrl Pts',(2.38551665840565,-1.72985067733577,4.72232156455017));
#61398=CARTESIAN_POINT('Ctrl Pts',(1.81704316028163,-2.51379290853814,4.6697011941798));
#61399=CARTESIAN_POINT('Ctrl Pts',(0.824428404318513,-2.99017030276568,
4.61708082380943));
#61400=CARTESIAN_POINT('Ctrl Pts',(-0.142797221412707,-2.9432434569701,
4.56446045343906));
#61401=CARTESIAN_POINT('Ctrl Pts',(-1.11002284714393,-2.89631661117452,
4.51184008306869));
#61402=CARTESIAN_POINT('Ctrl Pts',(-2.05185934264326,-2.32608552535581,
4.45921971269832));
#61403=CARTESIAN_POINT('Ctrl Pts',(-2.54177252355539,-1.49079359130735,
4.40659934232795));
#61404=CARTESIAN_POINT('Ctrl Pts',(-2.80377530896762,-1.04408421119714,
4.3784582672485));
#61405=CARTESIAN_POINT('Ctrl Pts',(-2.93652578376122,-0.52156611314212,
4.35031719216905));
#61406=CARTESIAN_POINT('Ctrl Pts',(-2.93739242931988,0.000540407572186541,
4.3221761170896));
#61407=CARTESIAN_POINT('Ctrl Pts',(-2.93753500859377,0.000882026442511374,
4.17782388291039));
#61408=CARTESIAN_POINT('Ctrl Pts',(-2.93605771780397,-0.543513730930775,
4.20716994094074));
#61409=CARTESIAN_POINT('Ctrl Pts',(-2.79100052624987,-1.08864123864977,
4.23651599897109));
#61410=CARTESIAN_POINT('Ctrl Pts',(-2.50727405993036,-1.54814577624058,
4.26586205700145));
#61411=CARTESIAN_POINT('Ctrl Pts',(-1.99809343933257,-2.37278088572845,
4.31852702066813));
#61412=CARTESIAN_POINT('Ctrl Pts',(-1.04230710189327,-2.92165405720309,
4.37119198433482));
#61413=CARTESIAN_POINT('Ctrl Pts',(-0.0734394371752462,-2.94580807344744,
4.4238569480015));
#61414=CARTESIAN_POINT('Ctrl Pts',(0.895428227542791,-2.9699620896918,4.47652191166818));
#61415=CARTESIAN_POINT('Ctrl Pts',(1.87737721953956,-2.46939695070584,4.52918687533487));
#61416=CARTESIAN_POINT('Ctrl Pts',(2.427016324523,-1.67115837574717,4.58185183900155));
#61417=CARTESIAN_POINT('Ctrl Pts',(2.97665542950643,-0.872919800788501,
4.63451680266824));
#61418=CARTESIAN_POINT('Ctrl Pts',(3.09398464747655,0.22299221014288,4.68718176633492));
#61419=CARTESIAN_POINT('Ctrl Pts',(2.725785936287,1.11949523708763,4.73984673000161));
#61420=CARTESIAN_POINT('Ctrl Pts',(2.35758722509745,2.01599826403239,4.79251169366829));
#61421=CARTESIAN_POINT('Ctrl Pts',(1.50386058474821,2.71309230699052,4.84517665733498));
#61422=CARTESIAN_POINT('Ctrl Pts',(0.551838293166775,2.8945903085884,4.89784162100166));
#61423=CARTESIAN_POINT('Ctrl Pts',(-0.400183998414646,3.07608831018627,
4.95050658466835));
#61424=CARTESIAN_POINT('Ctrl Pts',(-1.45050194122825,2.74199027042391,5.00317154833503));
#61425=CARTESIAN_POINT('Ctrl Pts',(-2.12271361651498,2.04383596665945,5.05583651200172));
#61426=CARTESIAN_POINT('Ctrl Pts',(-2.64172618991724,1.50479316935294,5.09649896897128));
#61427=CARTESIAN_POINT('Ctrl Pts',(-2.93533688440644,0.748724173372516,
5.13716142594084));
#61428=CARTESIAN_POINT('Ctrl Pts',(-2.94214529852914,-0.00261326515612426,
5.1778238829104));
#61429=CARTESIAN_POINT('Origin',(0.,0.,0.));
#61430=CARTESIAN_POINT('',(-2.94474230559933,0.0020353165097306,6.3221761170896));
#61431=CARTESIAN_POINT('',(-2.94552589459255,0.00164462538419303,6.1778238829104));
#61432=CARTESIAN_POINT('',(-2.942,-3.60291088309151E-16,0.));
#61433=CARTESIAN_POINT('Ctrl Pts',(-2.94474230559933,0.0020353165097306,
6.3221761170896));
#61434=CARTESIAN_POINT('Ctrl Pts',(-2.94577608567865,0.132578411608025,
6.31509496994683));
#61435=CARTESIAN_POINT('Ctrl Pts',(-2.93783733482844,0.262995037552802,
6.30801382280405));
#61436=CARTESIAN_POINT('Ctrl Pts',(-2.92049520368276,0.39214902611321,6.30093267566128));
#61437=CARTESIAN_POINT('Ctrl Pts',(-2.79162493090094,1.35189898976081,6.24831230529091));
#61438=CARTESIAN_POINT('Ctrl Pts',(-2.1434950231737,2.24192544902223,6.19569193492054));
#61439=CARTESIAN_POINT('Ctrl Pts',(-1.26962729970534,2.65915768867859,6.14307156455017));
#61440=CARTESIAN_POINT('Ctrl Pts',(-0.395759576236975,3.07638992833495,
6.0904511941798));
#61441=CARTESIAN_POINT('Ctrl Pts',(0.70384596297251,3.02082794838624,6.03783082380943));
#61442=CARTESIAN_POINT('Ctrl Pts',(1.53120548099802,2.51763437940803,5.98521045343906));
#61443=CARTESIAN_POINT('Ctrl Pts',(2.35856499902354,2.0144408104298,5.93259008306869));
#61444=CARTESIAN_POINT('Ctrl Pts',(2.91367849586509,1.06361565242206,5.87996971269832));
#61445=CARTESIAN_POINT('Ctrl Pts',(2.9451489575673,0.0957638301017936,5.82734934232795));
#61446=CARTESIAN_POINT('Ctrl Pts',(2.97661941926951,-0.872087992218468,
5.77472897195758));
#61447=CARTESIAN_POINT('Ctrl Pts',(2.48444684583239,-1.85696647885126,5.72210860158721));
#61448=CARTESIAN_POINT('Ctrl Pts',(1.69152388176343,-2.41284480454905,5.66948823121684));
#61449=CARTESIAN_POINT('Ctrl Pts',(0.898600917694462,-2.96872313024685,
5.61686786084646));
#61450=CARTESIAN_POINT('Ctrl Pts',(-0.19507243700635,-3.09560129500965,
5.56424749047609));
#61451=CARTESIAN_POINT('Ctrl Pts',(-1.09419888335647,-2.73601935246765,
5.51162712010572));
#61452=CARTESIAN_POINT('Ctrl Pts',(-1.9933253297066,-2.37643740992565,5.45900674973535));
#61453=CARTESIAN_POINT('Ctrl Pts',(-2.69790486770603,-1.53039536007885,
5.40638637936499));
#61454=CARTESIAN_POINT('Ctrl Pts',(-2.88885105295217,-0.581044479598858,
5.35376600899461));
#61455=CARTESIAN_POINT('Ctrl Pts',(-2.92706166295704,-0.391068040923041,
5.34323604502627));
#61456=CARTESIAN_POINT('Ctrl Pts',(-2.94470393564848,-0.196954622309047,
5.33270608105794));
#61457=CARTESIAN_POINT('Ctrl Pts',(-2.94294893056736,-0.00252441656932667,
5.3221761170896));
#61458=CARTESIAN_POINT('Ctrl Pts',(-2.94214529852914,-0.00261326515612426,
5.1778238829104));
#61459=CARTESIAN_POINT('Ctrl Pts',(-2.94415496646843,-0.224388664623296,
5.18982638960752));
#61460=CARTESIAN_POINT('Ctrl Pts',(-2.92117618657372,-0.445751813963285,
5.20182889630465));
#61461=CARTESIAN_POINT('Ctrl Pts',(-2.87162987121487,-0.660999575716158,
5.21383140300177));
#61462=CARTESIAN_POINT('Ctrl Pts',(-2.65422904286817,-1.60547024656074,
5.26649636666845));
#61463=CARTESIAN_POINT('Ctrl Pts',(-1.92532197841492,-2.43220102048334,
5.31916133033513));
#61464=CARTESIAN_POINT('Ctrl Pts',(-1.01552544630456,-2.76620437138433,
5.37182629400182));
#61465=CARTESIAN_POINT('Ctrl Pts',(-0.105728914194198,-3.10020772228531,
5.4244912576685));
#61466=CARTESIAN_POINT('Ctrl Pts',(0.984957085573281,-2.94148365016469,
5.47715622133519));
#61467=CARTESIAN_POINT('Ctrl Pts',(1.761820540694,-2.36202602414577,5.52982118500188));
#61468=CARTESIAN_POINT('Ctrl Pts',(2.53868399581473,-1.78256839812686,5.58248614866856));
#61469=CARTESIAN_POINT('Ctrl Pts',(3.0017249062887,-0.782377218209647,5.63515111233524));
#61470=CARTESIAN_POINT('Ctrl Pts',(2.94091774630216,0.184882032222853,5.68781607600193));
#61471=CARTESIAN_POINT('Ctrl Pts',(2.88011058631563,1.15214128265535,5.74048103966861));
#61472=CARTESIAN_POINT('Ctrl Pts',(2.2954553558686,2.08646860360313,5.7931460033353));
#61473=CARTESIAN_POINT('Ctrl Pts',(1.45213925422783,2.56407295970403,5.84581096700198));
#61474=CARTESIAN_POINT('Ctrl Pts',(0.60882315258705,3.04167731580494,5.89847593066867));
#61475=CARTESIAN_POINT('Ctrl Pts',(-0.493153820247473,3.06255870705896,
5.95114089433535));
#61476=CARTESIAN_POINT('Ctrl Pts',(-1.35395830631657,2.6172457777424,6.00380585800203));
#61477=CARTESIAN_POINT('Ctrl Pts',(-2.21476279238567,2.17193284842583,6.05647082166872));
#61478=CARTESIAN_POINT('Ctrl Pts',(-2.83439479168936,1.26042559853868,6.10913578533541));
#61479=CARTESIAN_POINT('Ctrl Pts',(-2.93180238522596,0.296164363719765,
6.16180074900209));
#61480=CARTESIAN_POINT('Ctrl Pts',(-2.94168102690256,0.198373309905978,
6.1671417936382));
#61481=CARTESIAN_POINT('Ctrl Pts',(-2.94618853440423,0.100039675683843,
6.1724828382743));
#61482=CARTESIAN_POINT('Ctrl Pts',(-2.94552589459255,0.00164462538419303,
6.1778238829104));
#61483=CARTESIAN_POINT('Origin',(0.,0.,0.));
#61484=CARTESIAN_POINT('',(-2.93737184280031,0.000478285809368539,7.32217611708959));
#61485=CARTESIAN_POINT('',(-2.93765213932985,0.00105817779144944,7.17782388291039));
#61486=CARTESIAN_POINT('',(-2.942,-3.60291088309151E-16,0.));
#61487=CARTESIAN_POINT('Ctrl Pts',(-2.93737184280031,0.000478285809368539,
7.32217611708959));
#61488=CARTESIAN_POINT('Ctrl Pts',(-2.93804459091945,0.458606303769958,
7.29748385883571));
#61489=CARTESIAN_POINT('Ctrl Pts',(-2.83719423177179,0.916453996322869,
7.27279160058183));
#61490=CARTESIAN_POINT('Ctrl Pts',(-2.63324974290992,1.32252368027208,7.24809934232795));
#61491=CARTESIAN_POINT('Ctrl Pts',(-2.198634389848,2.18787738530332,7.19547897195758));
#61492=CARTESIAN_POINT('Ctrl Pts',(-1.29583121079705,2.81808837804428,7.14285860158721));
#61493=CARTESIAN_POINT('Ctrl Pts',(-0.333697177699206,2.92774986756231,
7.09023823121684));
#61494=CARTESIAN_POINT('Ctrl Pts',(0.628436855398639,3.03741135708034,7.03761786084647));
#61495=CARTESIAN_POINT('Ctrl Pts',(1.64990174254338,2.62652334337548,6.9849974904761));
#61496=CARTESIAN_POINT('Ctrl Pts',(2.26810159307568,1.88116672756646,6.93237712010573));
#61497=CARTESIAN_POINT('Ctrl Pts',(2.886301443608,1.13581011175742,6.87975674973536));
#61498=CARTESIAN_POINT('Ctrl Pts',(3.10123625752784,0.055984893844227,6.82713637936498));
#61499=CARTESIAN_POINT('Ctrl Pts',(2.81556743521199,-0.869283101865742,
6.77451600899461));
#61500=CARTESIAN_POINT('Ctrl Pts',(2.52989861289615,-1.7945510975757,6.72189563862424));
#61501=CARTESIAN_POINT('Ctrl Pts',(1.74362615434463,-2.56526187108243,6.66927526825387));
#61502=CARTESIAN_POINT('Ctrl Pts',(0.812833183747132,-2.8323797960046,6.6166548978835));
#61503=CARTESIAN_POINT('Ctrl Pts',(-0.117959786850361,-3.09949772092676,
6.56403452751313));
#61504=CARTESIAN_POINT('Ctrl Pts',(-1.19327326949384,-2.86302279726437,
6.51141415714276));
#61505=CARTESIAN_POINT('Ctrl Pts',(-1.92612469189739,-2.23004860141629,
6.45879378677239));
#61506=CARTESIAN_POINT('Ctrl Pts',(-2.56035596550109,-1.68225403062272,
6.41325456354479));
#61507=CARTESIAN_POINT('Ctrl Pts',(-2.93809401248361,-0.83749407451141,
6.3677153403172));
#61508=CARTESIAN_POINT('Ctrl Pts',(-2.94474230559933,0.0020353165097306,
6.3221761170896));
#61509=CARTESIAN_POINT('Ctrl Pts',(-2.94552589459255,0.00164462538419303,
6.1778238829104));
#61510=CARTESIAN_POINT('Ctrl Pts',(-2.93965462503178,-0.87017722046166,
6.22514780194098));
#61511=CARTESIAN_POINT('Ctrl Pts',(-2.52789003171806,-1.74682066505967,
6.27247172097156));
#61512=CARTESIAN_POINT('Ctrl Pts',(-1.85003983495055,-2.2935847848838,6.31979564000214));
#61513=CARTESIAN_POINT('Ctrl Pts',(-1.095686503369,-2.90205747891776,6.37246060366883));
#61514=CARTESIAN_POINT('Ctrl Pts',(-0.0117966524363787,-3.10198764723502,
6.42512556733551));
#61515=CARTESIAN_POINT('Ctrl Pts',(0.910000294361383,-2.80269121035772,
6.4777905310022));
#61516=CARTESIAN_POINT('Ctrl Pts',(1.83179724115916,-2.50339477348041,6.53045549466888));
#61517=CARTESIAN_POINT('Ctrl Pts',(2.59150128382206,-1.70487173140855,6.58312045833556));
#61518=CARTESIAN_POINT('Ctrl Pts',(2.8445267984577,-0.769315181970455,6.63578542200225));
#61519=CARTESIAN_POINT('Ctrl Pts',(3.09755231309333,0.166241367467632,6.68845038566893));
#61520=CARTESIAN_POINT('Ctrl Pts',(2.84389929970168,1.23883142427194,6.74111534933562));
#61521=CARTESIAN_POINT('Ctrl Pts',(2.19861937965545,1.96195091165853,6.79378031300231));
#61522=CARTESIAN_POINT('Ctrl Pts',(1.55333945960922,2.68507039904512,6.84644527666899));
#61523=CARTESIAN_POINT('Ctrl Pts',(0.51643263290838,3.05871931701401,6.89911024033567));
#61524=CARTESIAN_POINT('Ctrl Pts',(-0.441782179220013,2.91341844960141,
6.95177520400236));
#61525=CARTESIAN_POINT('Ctrl Pts',(-1.39999699134843,2.76811758218879,7.00444016766904));
#61526=CARTESIAN_POINT('Ctrl Pts',(-2.2795197889044,2.10386692939468,7.05710513133573));
#61527=CARTESIAN_POINT('Ctrl Pts',(-2.68141770473996,1.22195648411116,7.10977009500241));
#61528=CARTESIAN_POINT('Ctrl Pts',(-2.85452884366231,0.842087578115104,
7.13245469097174));
#61529=CARTESIAN_POINT('Ctrl Pts',(-2.93902534565796,0.421835844039577,
7.15513928694107));
#61530=CARTESIAN_POINT('Ctrl Pts',(-2.93765213932985,0.00105817779144944,
7.17782388291039));
#61531=CARTESIAN_POINT('Origin',(0.,0.,0.));
#61532=CARTESIAN_POINT('',(-2.94306537549688,-0.00250657139928612,8.3221761170896));
#61533=CARTESIAN_POINT('',(-2.94179645842688,-0.00262223567938445,8.17782388291039));
#61534=CARTESIAN_POINT('',(-2.942,-3.60291088309151E-16,0.));
#61535=CARTESIAN_POINT('Ctrl Pts',(-2.94306537549688,-0.00250657139928612,
8.3221761170896));
#61536=CARTESIAN_POINT('Ctrl Pts',(-2.93603346312234,0.778523040326291,
8.2798727477246));
#61537=CARTESIAN_POINT('Ctrl Pts',(-2.6155295502631,1.5646541741046,8.23756937835961));
#61538=CARTESIAN_POINT('Ctrl Pts',(-2.0584790752992,2.10849163858216,8.19526600899462));
#61539=CARTESIAN_POINT('Ctrl Pts',(-1.36557440251332,2.78496089461673,8.14264563862425));
#61540=CARTESIAN_POINT('Ctrl Pts',(-0.306675260078988,3.08654352280986,
8.09002526825387));
#61541=CARTESIAN_POINT('Ctrl Pts',(0.638669423716989,2.87666029635488,8.0374048978835));
#61542=CARTESIAN_POINT('Ctrl Pts',(1.58401410751295,2.66677706989991,7.98478452751313));
#61543=CARTESIAN_POINT('Ctrl Pts',(2.41580433267058,1.94542798879682,7.93216415714276));
#61544=CARTESIAN_POINT('Ctrl Pts',(2.75734311734437,1.03929400395132,7.87954378677239));
#61545=CARTESIAN_POINT('Ctrl Pts',(3.09888190201817,0.133160019105817,7.82692341640202));
#61546=CARTESIAN_POINT('Ctrl Pts',(2.95016924620815,-0.957758869482093,
7.77430304603165));
#61547=CARTESIAN_POINT('Ctrl Pts',(2.37855339098706,-1.73941279161662,7.72168267566128));
#61548=CARTESIAN_POINT('Ctrl Pts',(1.80693753576595,-2.52106671375116,7.66906230529091));
#61549=CARTESIAN_POINT('Ctrl Pts',(0.812418481133763,-2.99345566943229,
7.61644193492054));
#61550=CARTESIAN_POINT('Ctrl Pts',(-0.154610975618871,-2.94264651965433,
7.56382156455017));
#61551=CARTESIAN_POINT('Ctrl Pts',(-1.1216404323715,-2.89183736987637,7.5112011941798));
#61552=CARTESIAN_POINT('Ctrl Pts',(-2.06118029124457,-2.31783011463932,
7.45858082380943));
#61553=CARTESIAN_POINT('Ctrl Pts',(-2.54773645714466,-1.48057827836003,
7.40596045343906));
#61554=CARTESIAN_POINT('Ctrl Pts',(-2.80597476023112,-1.03620924430037,
7.37803234132257));
#61555=CARTESIAN_POINT('Ctrl Pts',(-2.93661093285418,-0.517686173583286,
7.35010422920608));
#61556=CARTESIAN_POINT('Ctrl Pts',(-2.93737184280031,0.000478285809368539,
7.32217611708959));
#61557=CARTESIAN_POINT('Ctrl Pts',(-2.93765213932985,0.00105817779144944,
7.17782388291039));
#61558=CARTESIAN_POINT('Ctrl Pts',(-2.93583728528984,-0.555049110608679,
7.20780425060775));
#61559=CARTESIAN_POINT('Ctrl Pts',(-2.78403605908896,-1.11207503097007,
7.23778461830511));
#61560=CARTESIAN_POINT('Ctrl Pts',(-2.48858495099342,-1.57801251517323,
7.26776498600247));
#61561=CARTESIAN_POINT('Ctrl Pts',(-1.96958124729618,-2.39650083140119,
7.32042994966915));
#61562=CARTESIAN_POINT('Ctrl Pts',(-1.00730080578659,-2.93390722608419,
7.37309491333584));
#61563=CARTESIAN_POINT('Ctrl Pts',(-0.0382136038189444,-2.94647556868157,
7.42575987700252));
#61564=CARTESIAN_POINT('Ctrl Pts',(0.930873598148709,-2.95904391127895,
7.47842484066921));
#61565=CARTESIAN_POINT('Ctrl Pts',(1.90676756057442,-2.44677420179069,7.53108980433588));
#61566=CARTESIAN_POINT('Ctrl Pts',(2.44682350205541,-1.64202110404938,7.58375476800257));
#61567=CARTESIAN_POINT('Ctrl Pts',(2.98687944353639,-0.837268006308086,
7.63641973166925));
#61568=CARTESIAN_POINT('Ctrl Pts',(3.09109736407267,0.25996847968624,7.68908469533594));
#61569=CARTESIAN_POINT('Ctrl Pts',(2.71220622763963,1.15200518015635,7.74174965900263));
#61570=CARTESIAN_POINT('Ctrl Pts',(2.33331509120659,2.04404188062646,7.79441462266931));
#61571=CARTESIAN_POINT('Ctrl Pts',(1.47131489780423,2.73087879557235,7.84707958633599));
#61572=CARTESIAN_POINT('Ctrl Pts',(0.517190633372317,2.90098128313613,7.89974455000268));
#61573=CARTESIAN_POINT('Ctrl Pts',(-0.436933631059594,3.07108377069992,
7.95240951366936));
#61574=CARTESIAN_POINT('Ctrl Pts',(-1.48318196652107,2.72445183088159,8.00507447733605));
#61575=CARTESIAN_POINT('Ctrl Pts',(-2.14699834174799,2.01831035197405,8.05773944100273));
#61576=CARTESIAN_POINT('Ctrl Pts',(-2.65153376339188,1.48160562142403,8.09776758830529));
#61577=CARTESIAN_POINT('Ctrl Pts',(-2.93514585523751,0.737219387421443,
8.13779573560784));
#61578=CARTESIAN_POINT('Ctrl Pts',(-2.94179645842688,-0.00262223567938445,
8.17782388291039));
#61579=CARTESIAN_POINT('Origin',(0.,0.,0.));
#61580=CARTESIAN_POINT('',(-2.94464008512449,0.00207742171232136,9.3221761170896));
#61581=CARTESIAN_POINT('',(-2.94577110767244,0.00147777103002609,9.1778238829104));
#61582=CARTESIAN_POINT('',(-2.942,-3.60291088309151E-16,0.));
#61583=CARTESIAN_POINT('Ctrl Pts',(-2.94464008512449,0.00207742171232136,
9.3221761170896));
#61584=CARTESIAN_POINT('Ctrl Pts',(-2.94572064417758,0.136558752036829,
9.31488200698387));
#61585=CARTESIAN_POINT('Ctrl Pts',(-2.93729508396668,0.270903986837675,
9.30758789687813));
#61586=CARTESIAN_POINT('Ctrl Pts',(-2.91889749004766,0.4038694541666,9.3002937867724));
#61587=CARTESIAN_POINT('Ctrl Pts',(-2.7861755826581,1.3630943679524,9.24767341640203));
#61588=CARTESIAN_POINT('Ctrl Pts',(-2.1344781113937,2.25051190295123,9.19505304603165));
#61589=CARTESIAN_POINT('Ctrl Pts',(-1.25894255572533,2.66423286046833,9.14243267566128));
#61590=CARTESIAN_POINT('Ctrl Pts',(-0.383407000056953,3.07795381798544,
9.08981230529091));
#61591=CARTESIAN_POINT('Ctrl Pts',(0.715966640015389,3.01797819802083,9.03719193492054));
#61592=CARTESIAN_POINT('Ctrl Pts',(1.54129954888374,2.51146745828537,8.98457156455017));
#61593=CARTESIAN_POINT('Ctrl Pts',(2.3666324577521,2.00495671854991,8.9319511941798));
#61594=CARTESIAN_POINT('Ctrl Pts',(2.91792463541645,1.05191085904358,8.87933082380943));
#61595=CARTESIAN_POINT('Ctrl Pts',(2.94550964776859,0.0839405046308018,
8.82671045343906));
#61596=CARTESIAN_POINT('Ctrl Pts',(2.97309466012074,-0.884029849781979,
8.77409008306869));
#61597=CARTESIAN_POINT('Ctrl Pts',(2.47697250716068,-1.86692469910122,8.72146971269832));
#61598=CARTESIAN_POINT('Ctrl Pts',(1.68182449914462,-2.41961555778857,8.66884934232795));
#61599=CARTESIAN_POINT('Ctrl Pts',(0.886676491128584,-2.97230641647591,
8.61622897195757));
#61600=CARTESIAN_POINT('Ctrl Pts',(-0.207497371943416,-3.09479328453138,
8.56360860158721));
#61601=CARTESIAN_POINT('Ctrl Pts',(-1.10517312337017,-2.73160492399537,
8.51098823121684));
#61602=CARTESIAN_POINT('Ctrl Pts',(-2.00284887479693,-2.36841656345936,
8.45836786084647));
#61603=CARTESIAN_POINT('Ctrl Pts',(-2.70402651457844,-1.51955297433185,
8.4057474904761));
#61604=CARTESIAN_POINT('Ctrl Pts',(-2.89116023290047,-0.56944323783011,
8.35312712010573));
#61605=CARTESIAN_POINT('Ctrl Pts',(-2.92785056302318,-0.383160187412328,
8.34281011910035));
#61606=CARTESIAN_POINT('Ctrl Pts',(-2.94478032747652,-0.192985093804385,
8.33249311809497));
#61607=CARTESIAN_POINT('Ctrl Pts',(-2.94306537549688,-0.00250657139928612,
8.3221761170896));
#61608=CARTESIAN_POINT('Ctrl Pts',(-2.94179645842688,-0.00262223567938445,
8.17782388291039));
#61609=CARTESIAN_POINT('Ctrl Pts',(-2.94389604226671,-0.236188947098698,
8.19046069927452));
#61610=CARTESIAN_POINT('Ctrl Pts',(-2.91839215134056,-0.469302718100354,
8.20309751563865));
#61611=CARTESIAN_POINT('Ctrl Pts',(-2.86352159037298,-0.695286025907358,
8.21573433200279));
#61612=CARTESIAN_POINT('Ctrl Pts',(-2.63484404877868,-1.63708990688444,
8.26839929566947));
#61613=CARTESIAN_POINT('Ctrl Pts',(-1.89610455059774,-2.45504665084187,
8.32106425933616));
#61614=CARTESIAN_POINT('Ctrl Pts',(-0.982379647459882,-2.77814844538783,
8.37372922300284));
#61615=CARTESIAN_POINT('Ctrl Pts',(-0.068654744322021,-3.1012502399338,
8.42639418666953));
#61616=CARTESIAN_POINT('Ctrl Pts',(1.02005556377276,-2.92949708506828,8.47905915033621));
#61617=CARTESIAN_POINT('Ctrl Pts',(1.78993539631662,-2.34079256521527,8.53172411400289));
#61618=CARTESIAN_POINT('Ctrl Pts',(2.55981522886048,-1.75208804536226,8.58438907766958));
#61619=CARTESIAN_POINT('Ctrl Pts',(3.01086458585342,-0.746432160521719,
8.63705404133626));
#61620=CARTESIAN_POINT('Ctrl Pts',(2.93849705553841,0.220030931794408,8.68971900500295));
#61621=CARTESIAN_POINT('Ctrl Pts',(2.86612952522341,1.18649402411053,8.74238396866963));
#61622=CARTESIAN_POINT('Ctrl Pts',(2.27034510760049,2.11376432390223,8.79504893233632));
#61623=CARTESIAN_POINT('Ctrl Pts',(1.42137896494728,2.58125171077128,8.847713896003));
#61624=CARTESIAN_POINT('Ctrl Pts',(0.572412822294062,3.04873909764032,8.90037885966968));
#61625=CARTESIAN_POINT('Ctrl Pts',(-0.529735045389435,3.05644357158669,
8.95304382333637));
#61626=CARTESIAN_POINT('Ctrl Pts',(-1.38515376586909,2.60087054680792,9.00570878700305));
#61627=CARTESIAN_POINT('Ctrl Pts',(-2.24057248634875,2.14529752202914,9.05837375066974));
#61628=CARTESIAN_POINT('Ctrl Pts',(-2.84926205962455,1.2264469985252,9.11103871433643));
#61629=CARTESIAN_POINT('Ctrl Pts',(-2.93513381881397,0.261090064936974,
9.16370367800311));
#61630=CARTESIAN_POINT('Ctrl Pts',(-2.94280828744918,0.174814884615283,
9.16841041297221));
#61631=CARTESIAN_POINT('Ctrl Pts',(-2.94630689264378,0.0881682471389342,
9.1731171479413));
#61632=CARTESIAN_POINT('Ctrl Pts',(-2.94577110767244,0.00147777103002609,
9.1778238829104));
#61633=CARTESIAN_POINT('Origin',(0.,0.,0.));
#61634=CARTESIAN_POINT('',(-2.93735377875815,0.0004158914717875,10.3221761170896));
#61635=CARTESIAN_POINT('',(-2.93779053274574,0.00122895754932335,10.1778238829104));
#61636=CARTESIAN_POINT('',(-2.942,-3.60291088309151E-16,0.));
#61637=CARTESIAN_POINT('Ctrl Pts',(-2.93735377875815,0.0004158914717875,
10.3221761170896));
#61638=CARTESIAN_POINT('Ctrl Pts',(-2.93794360094505,0.462502223744089,
10.2972708958728));
#61639=CARTESIAN_POINT('Ctrl Pts',(-2.83526550161259,0.924340675123848,
10.2723656746559));
#61640=CARTESIAN_POINT('Ctrl Pts',(-2.6279195904465,1.33308353810155,10.2474604534391));
#61641=CARTESIAN_POINT('Ctrl Pts',(-2.18983399605069,2.19668561771623,10.1948400830687));
#61642=CARTESIAN_POINT('Ctrl Pts',(-1.28450826872579,2.82326745826868,10.1422197126983));
#61643=CARTESIAN_POINT('Ctrl Pts',(-0.321941779407734,2.9290658210569,10.0895993423279));
#61644=CARTESIAN_POINT('Ctrl Pts',(0.640624709910309,3.03486418384512,10.0369789719576));
#61645=CARTESIAN_POINT('Ctrl Pts',(1.66043196122149,2.61987906886913,9.98435860158721));
#61646=CARTESIAN_POINT('Ctrl Pts',(2.27563478565877,1.87204685190273,9.93173823121684));
#61647=CARTESIAN_POINT('Ctrl Pts',(2.89083761009605,1.12421463493634,9.87911786084647));
#61648=CARTESIAN_POINT('Ctrl Pts',(3.10143600765941,0.0435353159795382,
9.82649749047609));
#61649=CARTESIAN_POINT('Ctrl Pts',(2.8120552331994,-0.880578479665677,9.77387712010572));
#61650=CARTESIAN_POINT('Ctrl Pts',(2.52267445873939,-1.8046922753109,9.72125674973535));
#61651=CARTESIAN_POINT('Ctrl Pts',(1.733314512256,-2.57224054764455,9.66863637936499));
#61652=CARTESIAN_POINT('Ctrl Pts',(0.801456763974427,-2.83561988794246,
9.61601600899462));
#61653=CARTESIAN_POINT('Ctrl Pts',(-0.130400984307143,-3.09899922824038,
9.56339563862425));
#61654=CARTESIAN_POINT('Ctrl Pts',(-1.20475653438691,-2.85820963650256,
9.51077526825387));
#61655=CARTESIAN_POINT('Ctrl Pts',(-1.93506113766943,-2.22229869434726,
9.4581548978835));
#61656=CARTESIAN_POINT('Ctrl Pts',(-2.5641326605009,-1.67453620870937,9.41282863761886));
#61657=CARTESIAN_POINT('Ctrl Pts',(-2.93792539338528,-0.833601734574448,
9.36750237735423));
#61658=CARTESIAN_POINT('Ctrl Pts',(-2.94464008512449,0.00207742171232136,
9.3221761170896));
#61659=CARTESIAN_POINT('Ctrl Pts',(-2.94577110767244,0.00147777103002609,
9.1778238829104));
#61660=CARTESIAN_POINT('Ctrl Pts',(-2.94031184592155,-0.881835546255158,
9.22578211160798));
#61661=CARTESIAN_POINT('Ctrl Pts',(-2.51599664630944,-1.76970025068938,
9.27374034030557));
#61662=CARTESIAN_POINT('Ctrl Pts',(-1.82248510748737,-2.31554023703778,
9.32169856900316));
#61663=CARTESIAN_POINT('Ctrl Pts',(-1.06091069186834,-2.91495026175178,
9.37436353266984));
#61664=CARTESIAN_POINT('Ctrl Pts',(0.0252920844727601,-3.1019069675073,
9.42702849633653));
#61665=CARTESIAN_POINT('Ctrl Pts',(0.943444704192239,-2.79161076199491,
9.47969346000322));
#61666=CARTESIAN_POINT('Ctrl Pts',(1.86159732391172,-2.48131455648253,9.5323584236699));
#61667=CARTESIAN_POINT('Ctrl Pts',(2.61169978700958,-1.67376543970224,9.58502338733658));
#61668=CARTESIAN_POINT('Ctrl Pts',(2.85352154222556,-0.735250545330611,
9.63768835100327));
#61669=CARTESIAN_POINT('Ctrl Pts',(3.09534329744155,0.203264349041017,9.69035331466995));
#61670=CARTESIAN_POINT('Ctrl Pts',(2.82888434477565,1.27274502100399,9.74301827833664));
#61671=CARTESIAN_POINT('Ctrl Pts',(2.17500480776272,1.98809774472063,9.79568324200333));
#61672=CARTESIAN_POINT('Ctrl Pts',(1.52112527074978,2.70345046843728,9.84834820567001));
#61673=CARTESIAN_POINT('Ctrl Pts',(0.479825149389799,3.06467524390761,9.90101316933669));
#61674=CARTESIAN_POINT('Ctrl Pts',(-0.476583929910364,2.90792818241875,
9.95367813300337));
#61675=CARTESIAN_POINT('Ctrl Pts',(-1.43299300921054,2.75118112092989,10.0063430966701));
#61676=CARTESIAN_POINT('Ctrl Pts',(-2.3045110464509,2.07646222248183,10.0590080603367));
#61677=CARTESIAN_POINT('Ctrl Pts',(-2.69583596380714,1.18980965393578,10.1116730240034));
#61678=CARTESIAN_POINT('Ctrl Pts',(-2.85967973895049,0.818577213506006,
10.1337233103058));
#61679=CARTESIAN_POINT('Ctrl Pts',(-2.93934508420187,0.410192546500391,
10.1557735966081));
#61680=CARTESIAN_POINT('Ctrl Pts',(-2.93779053274574,0.00122895754932335,
10.1778238829104));
#61681=CARTESIAN_POINT('Origin',(0.,0.,0.));
#61682=CARTESIAN_POINT('',(-2.94318142996902,-0.00248705772575741,11.3221761170896));
#61683=CARTESIAN_POINT('',(-2.94145083142593,-0.00261642954227547,11.1778238829104));
#61684=CARTESIAN_POINT('',(-2.942,-3.60291088309151E-16,0.));
#61685=CARTESIAN_POINT('Ctrl Pts',(-2.94318142996902,-0.00248705772575741,
11.3221761170896));
#61686=CARTESIAN_POINT('Ctrl Pts',(-2.93613735245544,0.782394524444463,
11.2796597847616));
#61687=CARTESIAN_POINT('Ctrl Pts',(-2.61204283140731,1.57241444895454,11.2371434524337));
#61688=CARTESIAN_POINT('Ctrl Pts',(-2.04999848462302,2.11673789269853,11.1946271201057));
#61689=CARTESIAN_POINT('Ctrl Pts',(-1.35438388023453,2.79042020824128,11.1420067497354));
#61690=CARTESIAN_POINT('Ctrl Pts',(-0.294282642636005,3.08774972424349,
11.089386379365));
#61691=CARTESIAN_POINT('Ctrl Pts',(0.65021190135765,2.87407334222539,11.0367660089946));
#61692=CARTESIAN_POINT('Ctrl Pts',(1.59470644535131,2.66039696020728,10.9841456386242));
#61693=CARTESIAN_POINT('Ctrl Pts',(2.42359429574009,1.93571468016887,10.9315252682539));
#61694=CARTESIAN_POINT('Ctrl Pts',(2.76149288344003,1.02821697529914,10.8789048978835));
#61695=CARTESIAN_POINT('Ctrl Pts',(3.09939147113997,0.120719270429434,10.8262845275131));
#61696=CARTESIAN_POINT('Ctrl Pts',(2.9463007961511,-0.969593859271576,10.7736641571428));
#61697=CARTESIAN_POINT('Ctrl Pts',(2.37155179497663,-1.74894687658982,10.7210437867724));
#61698=CARTESIAN_POINT('Ctrl Pts',(1.79680279380215,-2.52829989390807,10.668423416402));
#61699=CARTESIAN_POINT('Ctrl Pts',(0.800395466442055,-2.99669279884355,
10.6158030460317));
#61700=CARTESIAN_POINT('Ctrl Pts',(-0.166422238380945,-2.94200216382593,
10.5631826756613));
#61701=CARTESIAN_POINT('Ctrl Pts',(-1.13323994320395,-2.8873115288083,10.5105623052909));
#61702=CARTESIAN_POINT('Ctrl Pts',(-2.07046802548985,-2.30953735383759,
10.4579419349205));
#61703=CARTESIAN_POINT('Ctrl Pts',(-2.55365933589945,-1.47033910701379,
10.4053215645502));
#61704=CARTESIAN_POINT('Ctrl Pts',(-2.80815619982173,-1.02833338914462,
10.3776064153966));
#61705=CARTESIAN_POINT('Ctrl Pts',(-2.93669740996939,-0.513805263571333,
10.3498912662431));
#61706=CARTESIAN_POINT('Ctrl Pts',(-2.93735377875815,0.0004158914717875,
10.3221761170896));
#61707=CARTESIAN_POINT('Ctrl Pts',(-2.93779053274574,0.00122895754932335,
10.1778238829104));
#61708=CARTESIAN_POINT('Ctrl Pts',(-2.93563218928374,-0.566577199606596,
10.2084385602748));
#61709=CARTESIAN_POINT('Ctrl Pts',(-2.77690932929649,-1.13549932265473,
10.2390532376391));
#61710=CARTESIAN_POINT('Ctrl Pts',(-2.46954008606165,-1.60765366907442,
10.2696679150035));
#61711=CARTESIAN_POINT('Ctrl Pts',(-1.94078749348779,-2.41987818489459,
10.3223328786702));
#61712=CARTESIAN_POINT('Ctrl Pts',(-0.972150510867944,-2.9457409778909,
10.3749978423368));
#61713=CARTESIAN_POINT('Ctrl Pts',(-0.00298230764251388,-2.94672185015728,
10.4276628060035));
#61714=CARTESIAN_POINT('Ctrl Pts',(0.966185895582889,-2.94770272242366,
10.4803277696702));
#61715=CARTESIAN_POINT('Ctrl Pts',(1.93588531941386,-2.42380167396015,10.5329927333369));
#61716=CARTESIAN_POINT('Ctrl Pts',(2.46628089363149,-1.61264909700348,10.5856576970036));
#61717=CARTESIAN_POINT('Ctrl Pts',(2.99667646784912,-0.801496520046785,
10.6383226606703));
#61718=CARTESIAN_POINT('Ctrl Pts',(3.08776819245338,0.296907585403119,10.690987624337));
#61719=CARTESIAN_POINT('Ctrl Pts',(2.69823879520542,1.18435043817229,10.7436525880036));
#61720=CARTESIAN_POINT('Ctrl Pts',(2.30870939795745,2.07179329094149,10.7963175516703));
#61721=CARTESIAN_POINT('Ctrl Pts',(1.43855887885726,2.74827489102996,10.848982515337));
#61722=CARTESIAN_POINT('Ctrl Pts',(0.482469038528927,2.90695754754173,10.9016474790037));
#61723=CARTESIAN_POINT('Ctrl Pts',(-0.473620801799363,3.0656402040535,10.9543124426704));
#61724=CARTESIAN_POINT('Ctrl Pts',(-1.51564996335577,2.70652391698861,11.0069774063371));
#61725=CARTESIAN_POINT('Ctrl Pts',(-2.17097614256679,1.99249620947818,11.0596423700038));
#61726=CARTESIAN_POINT('Ctrl Pts',(-2.66116565955863,1.45839745352016,11.0990362076393));
#61727=CARTESIAN_POINT('Ctrl Pts',(-2.93498842496261,0.725719853723158,
11.1384300452748));
#61728=CARTESIAN_POINT('Ctrl Pts',(-2.94145083142593,-0.00261642954227547,
11.1778238829104));
#61729=CARTESIAN_POINT('Origin',(0.,0.,0.));
#61730=CARTESIAN_POINT('',(-2.9445363666432,0.00211803469319205,12.3221761170896));
#61731=CARTESIAN_POINT('',(-2.94599368555865,0.00130075687149912,12.1778238829104));
#61732=CARTESIAN_POINT('',(-2.942,-3.60291088309151E-16,0.));
#61733=CARTESIAN_POINT('Ctrl Pts',(-2.9445363666432,0.00211803469319205,
12.3221761170896));
#61734=CARTESIAN_POINT('Ctrl Pts',(-2.9456637214079,0.140538485345201,12.3146690440209));
#61735=CARTESIAN_POINT('Ctrl Pts',(-2.93673667551181,0.278812877817704,
12.3071619709522));
#61736=CARTESIAN_POINT('Ctrl Pts',(-2.91725274860024,0.415583368023806,
12.2996548978835));
#61737=CARTESIAN_POINT('Ctrl Pts',(-2.78068135240184,1.37426776932391,12.2470345275131));
#61738=CARTESIAN_POINT('Ctrl Pts',(-2.12542680364205,2.25906209195984,12.1944141571428));
#61739=CARTESIAN_POINT('Ctrl Pts',(-1.24823752065428,2.66926510338839,12.1417937867724));
#61740=CARTESIAN_POINT('Ctrl Pts',(-0.371048237666502,3.07946811481694,
12.089173416402));
#61741=CARTESIAN_POINT('Ctrl Pts',(0.728075779549269,3.01507981503809,12.0365530460316));
#61742=CARTESIAN_POINT('Ctrl Pts',(1.55136877770631,2.50526006508935,11.9839326756613));
#61743=CARTESIAN_POINT('Ctrl Pts',(2.37466177586334,1.99544031514062,11.9313123052909));
#61744=CARTESIAN_POINT('Ctrl Pts',(2.92212375496165,1.04018911502201,11.8786919349205));
#61745=CARTESIAN_POINT('Ctrl Pts',(2.9458228744686,0.0721158274039949,11.8260715645502));
#61746=CARTESIAN_POINT('Ctrl Pts',(2.96952199397554,-0.895957460214037,
11.7734511941798));
#61747=CARTESIAN_POINT('Ctrl Pts',(2.4694582538911,-1.87685283533148,11.7208308238094));
#61748=CARTESIAN_POINT('Ctrl Pts',(1.67209801460167,-2.42634732122405,11.6682104534391));
#61749=CARTESIAN_POINT('Ctrl Pts',(0.874737775312261,-2.9758418071166,11.6155900830687));
#61750=CARTESIAN_POINT('Ctrl Pts',(-0.219918963182118,-3.09393540378431,
11.5629697126983));
#61751=CARTESIAN_POINT('Ctrl Pts',(-1.11612955404462,-2.72714647754463,
11.510349342328));
#61752=CARTESIAN_POINT('Ctrl Pts',(-2.01234014490716,-2.36035755130494,
11.4577289719576));
#61753=CARTESIAN_POINT('Ctrl Pts',(-2.7101045881378,-1.50868610215784,11.4051086015872));
#61754=CARTESIAN_POINT('Ctrl Pts',(-2.89342282416388,-0.557832820042644,
11.3524882312168));
#61755=CARTESIAN_POINT('Ctrl Pts',(-2.9286231547134,-0.375252240171749,
11.3423841931744));
#61756=CARTESIAN_POINT('Ctrl Pts',(-2.94485546023631,-0.189014750280763,
11.332280155132));
#61757=CARTESIAN_POINT('Ctrl Pts',(-2.94318142996902,-0.00248705772575741,
11.3221761170896));
#61758=CARTESIAN_POINT('Ctrl Pts',(-2.94145083142593,-0.00261642954227547,
11.1778238829104));
#61759=CARTESIAN_POINT('Ctrl Pts',(-2.94362790824268,-0.247980760321293,
11.1910950089415));
#61760=CARTESIAN_POINT('Ctrl Pts',(-2.9154621622164,-0.492852393533084,
11.2043661349727));
#61761=CARTESIAN_POINT('Ctrl Pts',(-2.85500395443405,-0.729473081400432,
11.2176372610038));
#61762=CARTESIAN_POINT('Ctrl Pts',(-2.61508239022462,-1.6684755368126,11.2703022246705));
#61763=CARTESIAN_POINT('Ctrl Pts',(-1.86661606494013,-2.4775413196809,11.3229671883372));
#61764=CARTESIAN_POINT('Ctrl Pts',(-0.949093412422085,-2.7896953688222,
11.3756321520039));
#61765=CARTESIAN_POINT('Ctrl Pts',(-0.0315707599040525,-3.10184941796349,
11.4282971156705));
#61766=CARTESIAN_POINT('Ctrl Pts',(1.05500821984753,-2.91709173337779,11.4809620793372));
#61767=CARTESIAN_POINT('Ctrl Pts',(1.81779437152408,-2.31922447800469,11.5336270430039));
#61768=CARTESIAN_POINT('Ctrl Pts',(2.58058052320064,-1.7213572226316,11.5862920066706));
#61769=CARTESIAN_POINT('Ctrl Pts',(3.01957384680218,-0.710380396471107,
11.6389569703373));
#61770=CARTESIAN_POINT('Ctrl Pts',(2.93565629151018,0.255148376847553,11.691621934004));
#61771=CARTESIAN_POINT('Ctrl Pts',(2.85173873621817,1.22067715016623,11.7442868976707));
#61772=CARTESIAN_POINT('Ctrl Pts',(2.24491030203262,2.14075787064307,11.7969518613373));
#61773=CARTESIAN_POINT('Ctrl Pts',(1.39041548234847,2.59806145861508,11.849616825004));
#61774=CARTESIAN_POINT('Ctrl Pts',(0.535920662664327,3.05536504658708,11.9022817886707));
#61775=CARTESIAN_POINT('Ctrl Pts',(-0.566240542518395,3.04989150205426,
11.9549467523374));
#61776=CARTESIAN_POINT('Ctrl Pts',(-1.41615121076395,2.58412350821102,12.0076117160041));
#61777=CARTESIAN_POINT('Ctrl Pts',(-2.26606187900951,2.11835551436778,12.0602766796708));
#61778=CARTESIAN_POINT('Ctrl Pts',(-2.86372201031791,1.19229307121411,12.1129416433374));
#61779=CARTESIAN_POINT('Ctrl Pts',(-2.93804565964555,0.22597844177242,12.1656066070041));
#61780=CARTESIAN_POINT('Ctrl Pts',(-2.94379288681505,0.151256200025011,
12.1696790323062));
#61781=CARTESIAN_POINT('Ctrl Pts',(-2.94641083929854,0.0762932715455572,
12.1737514576083));
#61782=CARTESIAN_POINT('Ctrl Pts',(-2.94599368555865,0.00130075687149912,
12.1778238829104));
#61783=CARTESIAN_POINT('Origin',(0.,0.,0.));
#61784=CARTESIAN_POINT('',(-2.93733773658367,0.000353650820144602,13.3221761170896));
#61785=CARTESIAN_POINT('',(-2.93794966127546,0.0013934910171998,13.1778238829104));
#61786=CARTESIAN_POINT('',(-2.942,-3.60291088309151E-16,0.));
#61787=CARTESIAN_POINT('Ctrl Pts',(-2.93733773658367,0.000353650820144602,
13.3221761170896));
#61788=CARTESIAN_POINT('Ctrl Pts',(-2.93784318272048,0.466397170874405,
13.2970579329098));
#61789=CARTESIAN_POINT('Ctrl Pts',(-2.8333193685149,0.932226520914598,13.27193974873));
#61790=CARTESIAN_POINT('Ctrl Pts',(-2.62254748003497,1.34362161549686,13.2468215645502));
#61791=CARTESIAN_POINT('Ctrl Pts',(-2.18099904818651,2.20545788879211,13.1942011941798));
#61792=CARTESIAN_POINT('Ctrl Pts',(-1.27316460447925,2.82840106158337,13.1415808238094));
#61793=CARTESIAN_POINT('Ctrl Pts',(-0.31018098965669,2.93033473129373,13.0889604534391));
#61794=CARTESIAN_POINT('Ctrl Pts',(0.652802625165875,3.03226840100409,13.0363400830687));
#61795=CARTESIAN_POINT('Ctrl Pts',(1.67093541110377,2.61319256763355,12.9837197126983));
#61796=CARTESIAN_POINT('Ctrl Pts',(2.28313120153524,1.86289672775273,12.9310993423279));
#61797=CARTESIAN_POINT('Ctrl Pts',(2.89532699196672,1.1126008878719,12.8784789719576));
#61798=CARTESIAN_POINT('Ctrl Pts',(3.10158578689178,0.0310850414808014,
12.8258586015872));
#61799=CARTESIAN_POINT('Ctrl Pts',(2.80849777284497,-0.891859624755379,
12.7732382312168));
#61800=CARTESIAN_POINT('Ctrl Pts',(2.51540975879817,-1.81480429099155,12.7206178608465));
#61801=CARTESIAN_POINT('Ctrl Pts',(1.72297493577951,-2.57917777707278,12.6679974904761));
#61802=CARTESIAN_POINT('Ctrl Pts',(0.790067400131255,-2.83881430845519,
12.6153771201057));
#61803=CARTESIAN_POINT('Ctrl Pts',(-0.142840135516982,-3.0984508398376,
12.5627567497353));
#61804=CARTESIAN_POINT('Ctrl Pts',(-1.21622038379481,-2.85335041652122,
12.510136379365));
#61805=CARTESIAN_POINT('Ctrl Pts',(-1.94396638611522,-2.21451296488091,
12.4575160089946));
#61806=CARTESIAN_POINT('Ctrl Pts',(-2.56788867194677,-1.66681511174075,
12.4124027116929));
#61807=CARTESIAN_POINT('Ctrl Pts',(-2.93776159700942,-0.829711212970877,
12.3672894143913));
#61808=CARTESIAN_POINT('Ctrl Pts',(-2.9445363666432,0.00211803469319205,
12.3221761170896));
#61809=CARTESIAN_POINT('Ctrl Pts',(-2.94599368555865,0.00130075687149912,
12.1778238829104));
#61810=CARTESIAN_POINT('Ctrl Pts',(-2.94101617029297,-0.893516551252978,
12.226416421275));
#61811=CARTESIAN_POINT('Ctrl Pts',(-2.50391622116005,-1.79254618589271,
12.2750089596396));
#61812=CARTESIAN_POINT('Ctrl Pts',(-1.79466984706922,-2.33716467042755,
12.3236014980042));
#61813=CARTESIAN_POINT('Ctrl Pts',(-1.02598321781837,-2.92742633745608,
12.3762664616709));
#61814=CARTESIAN_POINT('Ctrl Pts',(0.0623772080302214,-3.10138285578342,
12.4289314253375));
#61815=CARTESIAN_POINT('Ctrl Pts',(0.976754244976282,-2.78013123936204,
12.4815963890042));
#61816=CARTESIAN_POINT('Ctrl Pts',(1.89113128192235,-2.45887962294065,12.5342613526709));
#61817=CARTESIAN_POINT('Ctrl Pts',(2.6315249299659,-1.64241987177053,12.5869263163376));
#61818=CARTESIAN_POINT('Ctrl Pts',(2.86210835815027,-0.701080799331296,
12.6395912800043));
#61819=CARTESIAN_POINT('Ctrl Pts',(3.09269178633465,0.240258273107937,12.692256243671));
#61820=CARTESIAN_POINT('Ctrl Pts',(2.81346499465986,1.30647666681628,12.7449212073377));
#61821=CARTESIAN_POINT('Ctrl Pts',(2.15107931219979,2.01396036610533,12.7975861710043));
#61822=CARTESIAN_POINT('Ctrl Pts',(1.48869362973973,2.72144406539436,12.850251134671));
#61823=CARTESIAN_POINT('Ctrl Pts',(0.443149056494409,3.07019307026412,12.9029160983377));
#61824=CARTESIAN_POINT('Ctrl Pts',(-0.511317558922748,2.90202221756343,
12.9555810620044));
#61825=CARTESIAN_POINT('Ctrl Pts',(-1.46578417433991,2.73385136486274,13.0082460256711));
#61826=CARTESIAN_POINT('Ctrl Pts',(-2.3291728319289,2.04876065459161,13.0609109893378));
#61827=CARTESIAN_POINT('Ctrl Pts',(-2.7098688231833,1.1574927237348,13.1135759530044));
#61828=CARTESIAN_POINT('Ctrl Pts',(-2.86467717936984,0.795062526234979,
13.1349919296398));
#61829=CARTESIAN_POINT('Ctrl Pts',(-2.93966715879244,0.398538727939818,
13.1564079062751));
#61830=CARTESIAN_POINT('Ctrl Pts',(-2.93794966127546,0.0013934910171998,
13.1778238829104));
#61831=CARTESIAN_POINT('Origin',(0.,0.,0.));
#61832=CARTESIAN_POINT('',(-2.94325266537063,-0.0024318079996577,14.3221761170896));
#61833=CARTESIAN_POINT('',(-2.94111188951679,-0.00259486169482749,14.1778238829104));
#61834=CARTESIAN_POINT('',(-2.942,-3.60291088309151E-16,0.));
#61835=CARTESIAN_POINT('Ctrl Pts',(-2.94325266537063,-0.0024318079996577,
14.3221761170896));
#61836=CARTESIAN_POINT('Ctrl Pts',(-2.93620194204164,0.786300619982285,
14.2794468217987));
#61837=CARTESIAN_POINT('Ctrl Pts',(-2.60854122084458,1.58016790859219,14.2367175265078));
#61838=CARTESIAN_POINT('Ctrl Pts',(-2.04150376744995,2.12493551247607,14.1939882312168));
#61839=CARTESIAN_POINT('Ctrl Pts',(-1.34320718641939,2.79580716825642,14.1413678608465));
#61840=CARTESIAN_POINT('Ctrl Pts',(-0.281884150596186,3.08890703892681,
14.0887474904761));
#61841=CARTESIAN_POINT('Ctrl Pts',(0.661753798897932,2.87144767774516,14.0361271201057));
#61842=CARTESIAN_POINT('Ctrl Pts',(1.60539174839208,2.65398831656351,13.9835067497354));
#61843=CARTESIAN_POINT('Ctrl Pts',(2.43134461155714,1.92596972352975,13.930886379365));
#61844=CARTESIAN_POINT('Ctrl Pts',(2.76559296922098,1.01711939779235,13.8782660089946));
#61845=CARTESIAN_POINT('Ctrl Pts',(3.09984132688481,0.108269072054953,13.8256456386242));
#61846=CARTESIAN_POINT('Ctrl Pts',(2.94238517904746,-0.981412986386104,
13.7730252682539));
#61847=CARTESIAN_POINT('Ctrl Pts',(2.36451469520878,-1.75845069530582,13.7204048978835));
#61848=CARTESIAN_POINT('Ctrl Pts',(1.7866442113701,-2.53548840422553,13.6677845275131));
#61849=CARTESIAN_POINT('Ctrl Pts',(0.788359391530092,-2.99988176362388,
13.6151641571428));
#61850=CARTESIAN_POINT('Ctrl Pts',(-0.178232238982059,-2.94131149038551,
13.5625437867724));
#61851=CARTESIAN_POINT('Ctrl Pts',(-1.14482386949421,-2.88274121714715,
13.509923416402));
#61852=CARTESIAN_POINT('Ctrl Pts',(-2.07972231067849,-2.30120731127206,
13.4573030460317));
#61853=CARTESIAN_POINT('Ctrl Pts',(-2.5595403212758,-1.46007567143488,13.4046826756613));
#61854=CARTESIAN_POINT('Ctrl Pts',(-2.81031856879004,-1.02045582826861,
13.3771804894707));
#61855=CARTESIAN_POINT('Ctrl Pts',(-2.9367843178467,-0.509922711901109,
13.3496783032802));
#61856=CARTESIAN_POINT('Ctrl Pts',(-2.93733773658367,0.000353650820144602,
13.3221761170896));
#61857=CARTESIAN_POINT('Ctrl Pts',(-2.93794966127546,0.0013934910171998,
13.1778238829104));
#61858=CARTESIAN_POINT('Ctrl Pts',(-2.9354435856223,-0.578098472832708,
13.2090728699418));
#61859=CARTESIAN_POINT('Ctrl Pts',(-2.76961959866241,-1.15891354184382,
13.2403218569731));
#61860=CARTESIAN_POINT('Ctrl Pts',(-2.45014221851649,-1.63706498032062,
13.2715708440045));
#61861=CARTESIAN_POINT('Ctrl Pts',(-1.91171629767549,-2.44290960207673,
13.3242358076712));
#61862=CARTESIAN_POINT('Ctrl Pts',(-0.936861131073665,-2.95715369414646,
13.3769007713379));
#61863=CARTESIAN_POINT('Ctrl Pts',(0.032249473718084,-2.94654692146698,
13.4295657350046));
#61864=CARTESIAN_POINT('Ctrl Pts',(1.00136007850986,-2.9359401487875,13.4822306986712));
#61865=CARTESIAN_POINT('Ctrl Pts',(1.96472612149158,-2.40048251135878,13.5348956623379));
#61866=CARTESIAN_POINT('Ctrl Pts',(2.48538560527679,-1.58304647931889,13.5875606260046));
#61867=CARTESIAN_POINT('Ctrl Pts',(3.00604508906198,-0.765610447279041,
13.6402255896713));
#61868=CARTESIAN_POINT('Ctrl Pts',(3.08399801365073,0.333803979371919,13.692890553338));
#61869=CARTESIAN_POINT('Ctrl Pts',(2.68388585052197,1.21652624548705,13.7455555170047));
#61870=CARTESIAN_POINT('Ctrl Pts',(2.28377368739319,2.0992485116022,13.7982204806713));
#61871=CARTESIAN_POINT('Ctrl Pts',(1.40559643654686,2.76527861718149,13.850885444338));
#61872=CARTESIAN_POINT('Ctrl Pts',(0.447678061833244,2.91251851826326,13.9035504080047));
#61873=CARTESIAN_POINT('Ctrl Pts',(-0.510240312880357,3.05975841934504,
13.9562153716714));
#61874=CARTESIAN_POINT('Ctrl Pts',(-1.54789981146125,2.68820811592931,14.0088803353381));
#61875=CARTESIAN_POINT('Ctrl Pts',(-2.1946428070508,1.96639671204873,14.0615452990048));
#61876=CARTESIAN_POINT('Ctrl Pts',(-2.67062249982462,1.435169358057,14.1003048269733));
#61877=CARTESIAN_POINT('Ctrl Pts',(-2.93486488519192,0.714225423327012,
14.1390643549419));
#61878=CARTESIAN_POINT('Ctrl Pts',(-2.94111188951679,-0.00259486169482749,
14.1778238829104));
#61879=CARTESIAN_POINT('Origin',(0.,0.,-1.84858989190501));
#61880=CARTESIAN_POINT('',(-2.37275986033066,-0.00196044888638088,14.651410108095));
#61881=CARTESIAN_POINT('',(-2.37517539399571,0.0009292342096269,14.848589891905));
#61882=CARTESIAN_POINT('',(-2.37175,-2.62313128856983E-13,-1.84858989190501));
#61883=CARTESIAN_POINT('',(-2.34668236863853,0.343918483395512,15.62825));
#61884=CARTESIAN_POINT('Ctrl Pts',(-2.37275986033066,-0.00196044888638126,
14.651410108095));
#61885=CARTESIAN_POINT('Ctrl Pts',(-2.37407562336888,-0.149148890039704,
14.6613011831744));
#61886=CARTESIAN_POINT('Ctrl Pts',(-2.29486163858049,-1.07797575416432,
14.7238126286243));
#61887=CARTESIAN_POINT('Ctrl Pts',(-1.07036982067409,-2.58532778276268,
14.8389444444444));
#61888=CARTESIAN_POINT('Ctrl Pts',(1.57881200919325,-2.30987053095853,14.9968055555556));
#61889=CARTESIAN_POINT('Ctrl Pts',(2.79654399706859,0.0566462213665858,
15.1546666666667));
#61890=CARTESIAN_POINT('Ctrl Pts',(1.48409012818578,2.37398300468726,15.3125277777778));
#61891=CARTESIAN_POINT('Ctrl Pts',(-1.17817012667699,2.53688639776398,15.4703888888889));
#61892=CARTESIAN_POINT('Ctrl Pts',(-2.23297482288527,1.11978691060522,15.5756296296296));
#61893=CARTESIAN_POINT('Ctrl Pts',(-2.34668236863854,0.343918483395395,
15.62825));
#61894=CARTESIAN_POINT('',(-0.439445221994505,2.33068358199182,15.62825));
#61895=CARTESIAN_POINT('Origin',(0.,0.,15.62825));
#61896=CARTESIAN_POINT('Ctrl Pts',(-2.37517539399571,0.000929234209626874,
14.848589891905));
#61897=CARTESIAN_POINT('Ctrl Pts',(-2.37154287511732,-0.72977569986937,
14.8978167399366));
#61898=CARTESIAN_POINT('Ctrl Pts',(-1.620069408967,-2.24871933567263,14.9997085516349));
#61899=CARTESIAN_POINT('Ctrl Pts',(0.958368222991996,-2.62865236842956,
15.1542653269999));
#61900=CARTESIAN_POINT('Ctrl Pts',(2.7277014223945,-0.634378452891388,15.3122602179999));
#61901=CARTESIAN_POINT('Ctrl Pts',(2.01676643438217,1.93930517753648,15.470255109));
#61902=CARTESIAN_POINT('Ctrl Pts',(0.331786659212352,2.47609764328476,15.5755850363333));
#61903=CARTESIAN_POINT('Ctrl Pts',(-0.439445221994538,2.33068358199181,
15.62825));
#61904=CARTESIAN_POINT('Origin',(0.,0.,-1.84858989190501));
#61905=CARTESIAN_POINT('',(-2.36799142649297,0.000285102424211894,13.651410108095));
#61906=CARTESIAN_POINT('',(-2.37103403261776,-0.00209189776527924,13.848589891905));
#61907=CARTESIAN_POINT('',(-2.37175,-2.62313128856983E-13,-1.84858989190501));
#61908=CARTESIAN_POINT('Ctrl Pts',(-2.36799142649297,0.000285102424211897,
13.651410108095));
#61909=CARTESIAN_POINT('Ctrl Pts',(-2.36754527731231,-0.41108402173757,
13.6789122942855));
#61910=CARTESIAN_POINT('Ctrl Pts',(-2.07052456040773,-1.61013525385437,
13.7590348508465));
#61911=CARTESIAN_POINT('Ctrl Pts',(-0.16923542984156,-2.79279215602584,
13.8917777777778));
#61912=CARTESIAN_POINT('Ctrl Pts',(2.24512421134353,-1.66965318578134,14.0496388888889));
#61913=CARTESIAN_POINT('Ctrl Pts',(2.62593313585052,0.965751391486786,14.2075));
#61914=CARTESIAN_POINT('Ctrl Pts',(0.628359679142483,2.72647005025058,14.3653611111111));
#61915=CARTESIAN_POINT('Ctrl Pts',(-1.77762972544941,2.06202090562868,14.5133311471428));
#61916=CARTESIAN_POINT('Ctrl Pts',(-2.36707578383325,0.633891398858792,
14.6086808128041));
#61917=CARTESIAN_POINT('Ctrl Pts',(-2.37275986033066,-0.00196044888638126,
14.651410108095));
#61918=CARTESIAN_POINT('Ctrl Pts',(-2.37103403261776,-0.00209189776527889,
13.848589891905));
#61919=CARTESIAN_POINT('Ctrl Pts',(-2.37284080801943,-0.20941258958213,
13.8624953276032));
#61920=CARTESIAN_POINT('Ctrl Pts',(-2.25333213139831,-1.19988405133594,
13.929065726968));
#61921=CARTESIAN_POINT('Ctrl Pts',(-0.869666078203209,-2.66015561356989,
14.0483010899995));
#61922=CARTESIAN_POINT('Ctrl Pts',(1.75267763866885,-2.18191305067097,14.2062959809995));
#61923=CARTESIAN_POINT('Ctrl Pts',(2.78512620401791,0.275629071355557,14.3642908719996));
#61924=CARTESIAN_POINT('Ctrl Pts',(1.29091271455523,2.48320730756548,14.5222857629997));
#61925=CARTESIAN_POINT('Ctrl Pts',(-1.37414448785656,2.43798182357128,14.6802806539997));
#61926=CARTESIAN_POINT('Ctrl Pts',(-2.35095938458833,0.884486526760038,
14.7890486969682));
#61927=CARTESIAN_POINT('Ctrl Pts',(-2.37542909742077,0.0519633377314283,
14.8451517762699));
#61928=CARTESIAN_POINT('Ctrl Pts',(-2.37517539399571,0.000929234209626874,
14.848589891905));
#61929=CARTESIAN_POINT('Origin',(0.,0.,-1.84858989190501));
#61930=CARTESIAN_POINT('',(-2.3737947408518,0.00170749448784205,12.651410108095));
#61931=CARTESIAN_POINT('',(-2.36848474137664,0.00112338963946246,12.848589891905));
#61932=CARTESIAN_POINT('',(-2.37175,-2.62313128856983E-13,-1.84858989190501));
#61933=CARTESIAN_POINT('Ctrl Pts',(-2.3737947408518,0.00170749448784207,
12.651410108095));
#61934=CARTESIAN_POINT('Ctrl Pts',(-2.36833312974404,-0.668887685031927,
12.6965234053967));
#61935=CARTESIAN_POINT('Ctrl Pts',(-1.72235411599047,-2.13088047848934,
12.7942570730687));
#61936=CARTESIAN_POINT('Ctrl Pts',(0.750172845833004,-2.69546828972993,
12.9446111111111));
#61937=CARTESIAN_POINT('Ctrl Pts',(2.66668266040929,-0.846825037914988,
13.1024722222222));
#61938=CARTESIAN_POINT('Ctrl Pts',(2.16784415239069,1.76882949166842,13.2603333333333));
#61939=CARTESIAN_POINT('Ctrl Pts',(-0.294517949969841,2.78236767093066,
13.4181944444444));
#61940=CARTESIAN_POINT('Ctrl Pts',(-2.10760963637491,1.5382497642797,13.548553369365));
#61941=CARTESIAN_POINT('Ctrl Pts',(-2.36839890163746,0.375995067988055,
13.6262919239152));
#61942=CARTESIAN_POINT('Ctrl Pts',(-2.36799142649297,0.000285102424211897,
13.651410108095));
#61943=CARTESIAN_POINT('Ctrl Pts',(-2.36848474137664,0.00112338963946246,
12.848589891905));
#61944=CARTESIAN_POINT('Ctrl Pts',(-2.36646442019019,-0.466045225337024,
12.8798388789364));
#61945=CARTESIAN_POINT('Ctrl Pts',(-2.00748312661735,-1.72341304420753,
12.9637528296344));
#61946=CARTESIAN_POINT('Ctrl Pts',(0.0306296239850783,-2.7985342282319,
13.1003317439992));
#61947=CARTESIAN_POINT('Ctrl Pts',(2.36053793034993,-1.50352574600393,13.2583266349992));
#61948=CARTESIAN_POINT('Ctrl Pts',(2.54906768788899,1.15541663986578,13.4163215259993));
#61949=CARTESIAN_POINT('Ctrl Pts',(0.42518914129335,2.76621565710669,13.5743164169993));
#61950=CARTESIAN_POINT('Ctrl Pts',(-1.86352481270074,1.94670562977947,13.7184058723013));
#61951=CARTESIAN_POINT('Ctrl Pts',(-2.36599788968529,0.57578658999839,13.8098303639365));
#61952=CARTESIAN_POINT('Ctrl Pts',(-2.37103403261776,-0.00209189776527889,
13.848589891905));
#61953=CARTESIAN_POINT('Origin',(0.,0.,-1.84858989190501));
#61954=CARTESIAN_POINT('',(-2.37270243253876,-0.00200498951788303,11.651410108095));
#61955=CARTESIAN_POINT('',(-2.37496958658182,0.00104863022067879,11.848589891905));
#61956=CARTESIAN_POINT('',(-2.37175,-2.62313128856983E-13,-1.84858989190501));
#61957=CARTESIAN_POINT('Ctrl Pts',(-2.37270243253876,-0.00200498951788284,
11.651410108095));
#61958=CARTESIAN_POINT('Ctrl Pts',(-2.37405198430164,-0.152377883745359,
11.6615141461374));
#61959=CARTESIAN_POINT('Ctrl Pts',(-2.29281607417404,-1.08441874324097,
11.7242385545502));
#61960=CARTESIAN_POINT('Ctrl Pts',(-1.05977053720295,-2.58943908287633,
11.8395833333333));
#61961=CARTESIAN_POINT('Ctrl Pts',(1.58766534266525,-2.30382879610199,11.9974444444444));
#61962=CARTESIAN_POINT('Ctrl Pts',(2.79707340746319,0.0684743370742143,
12.1553055555555));
#61963=CARTESIAN_POINT('Ctrl Pts',(1.47303233105958,2.37875683253439,12.3131666666667));
#61964=CARTESIAN_POINT('Ctrl Pts',(-1.18520769732058,2.53448043892505,12.4710277777778));
#61965=CARTESIAN_POINT('Ctrl Pts',(-2.31706196946124,1.00613052370996,12.5837755915872));
#61966=CARTESIAN_POINT('Ctrl Pts',(-2.37470357962243,0.113297808503467,
12.6439030350263));
#61967=CARTESIAN_POINT('Ctrl Pts',(-2.3737947408518,0.00170749448784207,
12.651410108095));
#61968=CARTESIAN_POINT('Ctrl Pts',(-2.37496958658182,0.00104863022067909,
11.848589891905));
#61969=CARTESIAN_POINT('Ctrl Pts',(-2.37095686672064,-0.72032558818314,
11.8971824302696));
#61970=CARTESIAN_POINT('Ctrl Pts',(-1.63667192852724,-2.23060698037937,
11.9984399323009));
#61971=CARTESIAN_POINT('Ctrl Pts',(0.927689321261817,-2.64047796075702,
12.1523623979988));
#61972=CARTESIAN_POINT('Ctrl Pts',(2.71833714731268,-0.66586366962402,12.3103572889989));
#61973=CARTESIAN_POINT('Ctrl Pts',(2.04302496870488,1.91279385105346,12.468352179999));
#61974=CARTESIAN_POINT('Ctrl Pts',(-0.48563275555883,2.75624604578475,12.626347070999));
#61975=CARTESIAN_POINT('Ctrl Pts',(-2.16074812800628,1.4270578867686,12.7530929749677));
#61976=CARTESIAN_POINT('Ctrl Pts',(-2.36986933510064,0.32128967640745,12.8271739152697));
#61977=CARTESIAN_POINT('Ctrl Pts',(-2.36848474137664,0.00112338963946246,
12.848589891905));
#61978=CARTESIAN_POINT('Origin',(0.,0.,-1.84858989190501));
#61979=CARTESIAN_POINT('',(-2.3680043592011,0.000335278925106314,10.651410108095));
#61980=CARTESIAN_POINT('',(-2.37130727717011,-0.00210928510120167,10.848589891905));
#61981=CARTESIAN_POINT('',(-2.37175,-2.62313128856983E-13,-1.84858989190501));
#61982=CARTESIAN_POINT('Ctrl Pts',(-2.3680043592011,0.000335278925106194,
10.651410108095));
#61983=CARTESIAN_POINT('Ctrl Pts',(-2.36747521485208,-0.414214015593381,
10.6791252572485));
#61984=CARTESIAN_POINT('Ctrl Pts',(-2.06710351553143,-1.61654972761244,
10.7594607767724));
#61985=CARTESIAN_POINT('Ctrl Pts',(-0.158018739337926,-2.79344562132492,
10.8924166666667));
#61986=CARTESIAN_POINT('Ctrl Pts',(2.25180017160661,-1.66063371893121,11.0502777777778));
#61987=CARTESIAN_POINT('Ctrl Pts',(2.62205116590109,0.976297109112734,11.2081388888889));
#61988=CARTESIAN_POINT('Ctrl Pts',(0.617379419647229,2.72894686881467,11.366));
#61989=CARTESIAN_POINT('Ctrl Pts',(-1.78238141625357,2.05587933285381,11.5137570730687));
#61990=CARTESIAN_POINT('Ctrl Pts',(-2.36702371369352,0.630742424660346,
11.608893775767));
#61991=CARTESIAN_POINT('Ctrl Pts',(-2.37270243253876,-0.00200498951788284,
11.651410108095));
#61992=CARTESIAN_POINT('Ctrl Pts',(-2.37130727717011,-0.00210928510120129,
10.848589891905));
#61993=CARTESIAN_POINT('Ctrl Pts',(-2.37306236960384,-0.199914469168129,
10.8618610179362));
#61994=CARTESIAN_POINT('Ctrl Pts',(-2.26024839139859,-1.18071373741556,
10.927797107634));
#61995=CARTESIAN_POINT('Ctrl Pts',(-0.90141796228012,-2.64956165719617,
11.0463981609985));
#61996=CARTESIAN_POINT('Ctrl Pts',(1.72648179491819,-2.20272375262492,11.2043930519985));
#61997=CARTESIAN_POINT('Ctrl Pts',(2.7881905800153,0.242331605070017,11.3623879429986));
#61998=CARTESIAN_POINT('Ctrl Pts',(1.32057126786748,2.46755402056041,11.5203828339987));
#61999=CARTESIAN_POINT('Ctrl Pts',(-1.34501422335496,2.45431621031658,11.6783777249987));
#62000=CARTESIAN_POINT('Ctrl Pts',(-2.34590203170026,0.903460530701682,
11.7877800776342));
#62001=CARTESIAN_POINT('Ctrl Pts',(-2.37530588310888,0.0615052912262518,
11.8445174666029));
#62002=CARTESIAN_POINT('Ctrl Pts',(-2.37496958658182,0.00104863022067909,
11.848589891905));
#62003=CARTESIAN_POINT('Origin',(0.,0.,-1.84858989190501));
#62004=CARTESIAN_POINT('',(-2.37387835550442,0.0016747535505271,9.65141010809499));
#62005=CARTESIAN_POINT('',(-2.36835645684558,0.000990747813277848,9.84858989190503));
#62006=CARTESIAN_POINT('',(-2.37175,-2.62313128856983E-13,-1.84858989190501));
#62007=CARTESIAN_POINT('Ctrl Pts',(-2.37387835550442,0.00167475355052717,
9.65141010809499));
#62008=CARTESIAN_POINT('Ctrl Pts',(-2.36846517734921,-0.672024104003181,
9.69673636835963));
#62009=CARTESIAN_POINT('Ctrl Pts',(-1.71729169385484,-2.1369916722257,9.79468299899462));
#62010=CARTESIAN_POINT('Ctrl Pts',(0.760987165659879,-2.69243512365168,
9.94525));
#62011=CARTESIAN_POINT('Ctrl Pts',(2.6700603672968,-0.836113626465368,10.1031111111111));
#62012=CARTESIAN_POINT('Ctrl Pts',(2.16072649637127,1.7775177549783,10.2609722222222));
#62013=CARTESIAN_POINT('Ctrl Pts',(-0.305685313585232,2.78116249982291,
10.4188333333333));
#62014=CARTESIAN_POINT('Ctrl Pts',(-2.11081288774265,1.53182193243431,10.5489792952909));
#62015=CARTESIAN_POINT('Ctrl Pts',(-2.36847985572451,0.37285508129321,10.6265048868781));
#62016=CARTESIAN_POINT('Ctrl Pts',(-2.3680043592011,0.000335278925106194,
10.651410108095));
#62017=CARTESIAN_POINT('Ctrl Pts',(-2.36835645684558,0.00099074781327764,
9.84858989190503));
#62018=CARTESIAN_POINT('Ctrl Pts',(-2.36661646666674,-0.456757128880904,
9.87920456926939));
#62019=CARTESIAN_POINT('Ctrl Pts',(-2.01853982608692,-1.70439405627733,
9.96248421030043));
#62020=CARTESIAN_POINT('Ctrl Pts',(-0.00283249851198579,-2.79870028674429,
10.0984288149982));
#62021=CARTESIAN_POINT('Ctrl Pts',(2.34239313895008,-1.53164150527581,10.2564237059982));
#62022=CARTESIAN_POINT('Ctrl Pts',(2.56269918704329,1.12485741087042,10.4144185969983));
#62023=CARTESIAN_POINT('Ctrl Pts',(0.458233353927178,2.76093344928963,10.5724134879983));
#62024=CARTESIAN_POINT('Ctrl Pts',(-1.85023633825226,1.96536160231837,10.7171372529672));
#62025=CARTESIAN_POINT('Ctrl Pts',(-2.36609748365237,0.585053046589831,
10.8091960542695));
#62026=CARTESIAN_POINT('Ctrl Pts',(-2.37130727717011,-0.00210928510120129,
10.848589891905));
#62027=CARTESIAN_POINT('Origin',(0.,0.,-1.84858989190501));
#62028=CARTESIAN_POINT('',(-2.37260887298938,-0.00202072084187682,8.65141010809499));
#62029=CARTESIAN_POINT('',(-2.3747901511292,0.00119133359606532,8.84858989190503));
#62030=CARTESIAN_POINT('',(-2.37175,-2.62313128856983E-13,-1.84858989190501));
#62031=CARTESIAN_POINT('Ctrl Pts',(-2.37260887298937,-0.00202072084187674,
8.65141010809499));
#62032=CARTESIAN_POINT('Ctrl Pts',(-2.37399141457934,-0.155578652695773,
8.66172710910036));
#62033=CARTESIAN_POINT('Ctrl Pts',(-2.29073220490892,-1.09084435213441,
8.72466448047611));
#62034=CARTESIAN_POINT('Ctrl Pts',(-1.04936735270146,-2.59367240037321,
8.84022222222223));
#62035=CARTESIAN_POINT('Ctrl Pts',(1.59690068918271,-2.29743695240177,8.99808333333332));
#62036=CARTESIAN_POINT('Ctrl Pts',(2.79677599470576,0.0797019247629725,
9.15594444444445));
#62037=CARTESIAN_POINT('Ctrl Pts',(1.46347155312646,2.38465078671139,9.31380555555555));
#62038=CARTESIAN_POINT('Ctrl Pts',(-1.19537219008389,2.52970229247383,9.47166666666666));
#62039=CARTESIAN_POINT('Ctrl Pts',(-2.31895585283185,0.999716542450464,
9.58420151751315));
#62040=CARTESIAN_POINT('Ctrl Pts',(-2.37474946901026,0.110089469797055,
9.64411599798926));
#62041=CARTESIAN_POINT('Ctrl Pts',(-2.37387835550442,0.00167475355052717,
9.65141010809499));
#62042=CARTESIAN_POINT('Ctrl Pts',(-2.3747901511292,0.00119133359606537,
8.84858989190503));
#62043=CARTESIAN_POINT('Ctrl Pts',(-2.37038906205444,-0.71090872088079,
8.89654812060261));
#62044=CARTESIAN_POINT('Ctrl Pts',(-1.65267775677864,-2.21269450774448,
8.99717131296688));
#62045=CARTESIAN_POINT('Ctrl Pts',(0.896053003445084,-2.6513808351669,9.15045946899784));
#62046=CARTESIAN_POINT('Ctrl Pts',(2.71018167460651,-0.698316982967359,
9.30845435999788));
#62047=CARTESIAN_POINT('Ctrl Pts',(2.06574861445826,1.88823038317285,9.46644925099794));
#62048=CARTESIAN_POINT('Ctrl Pts',(-0.45264386973844,2.76185532663481,9.62444414199799));
#62049=CARTESIAN_POINT('Ctrl Pts',(-2.15199374797492,1.44623886325989,9.75182435563369));
#62050=CARTESIAN_POINT('Ctrl Pts',(-2.36960968846224,0.330684626839437,
9.8265396056027));
#62051=CARTESIAN_POINT('Ctrl Pts',(-2.36835645684558,0.00099074781327764,
9.84858989190503));
#62052=CARTESIAN_POINT('Origin',(0.,0.,-1.84858989190501));
#62053=CARTESIAN_POINT('',(-2.36801892187683,0.000385579322849399,7.65141010809499));
#62054=CARTESIAN_POINT('',(-2.37158591103805,-0.00211396583053219,7.84858989190503));
#62055=CARTESIAN_POINT('',(-2.37175,-2.62313128856983E-13,-1.84858989190501));
#62056=CARTESIAN_POINT('Ctrl Pts',(-2.36801892187683,0.000385579322849869,
7.65141010809499));
#62057=CARTESIAN_POINT('Ctrl Pts',(-2.36740549965901,-0.417342685994756,
7.67933822021147));
#62058=CARTESIAN_POINT('Ctrl Pts',(-2.06366306314178,-1.62296175556451,
7.75988670269832));
#62059=CARTESIAN_POINT('Ctrl Pts',(-0.146803886877873,-2.79405744038503,
7.89305555555557));
#62060=CARTESIAN_POINT('Ctrl Pts',(2.25844822171206,-1.65158105802259,8.05091666666665));
#62061=CARTESIAN_POINT('Ctrl Pts',(2.61811094239596,0.986814802625037,8.20877777777778));
#62062=CARTESIAN_POINT('Ctrl Pts',(0.606419780073446,2.73140319464357,8.36663888888888));
#62063=CARTESIAN_POINT('Ctrl Pts',(-1.7871649975578,2.04969182184781,8.51418299899463));
#62064=CARTESIAN_POINT('Ctrl Pts',(-2.36693996130543,0.627621353124904,
8.60910673873));
#62065=CARTESIAN_POINT('Ctrl Pts',(-2.37260887298937,-0.00202072084187674,
8.65141010809499));
#62066=CARTESIAN_POINT('Ctrl Pts',(-2.37158591103805,-0.002113965830532,
7.84858989190503));
#62067=CARTESIAN_POINT('Ctrl Pts',(-2.37327853101496,-0.190408271679788,
7.86122670826915));
#62068=CARTESIAN_POINT('Ctrl Pts',(-2.26703071089283,-1.16154754141212,
7.92652848829996));
#62069=CARTESIAN_POINT('Ctrl Pts',(-0.9330321424437,-2.63859476601473,8.04449523199746));
#62070=CARTESIAN_POINT('Ctrl Pts',(1.70002224901497,-2.22320841823872,8.2024901229975));
#62071=CARTESIAN_POINT('Ctrl Pts',(2.79088864512093,0.208978201275766,8.36048501399757));
#62072=CARTESIAN_POINT('Ctrl Pts',(1.34997937336987,2.45158867054595,8.51847990499762));
#62073=CARTESIAN_POINT('Ctrl Pts',(-1.31557386100644,2.47022200101732,8.67647479599767));
#62074=CARTESIAN_POINT('Ctrl Pts',(-2.34084261733164,0.922522196646213,
8.78651145830014));
#62075=CARTESIAN_POINT('Ctrl Pts',(-2.37522208450983,0.0710785316625285,
8.84388315693593));
#62076=CARTESIAN_POINT('Ctrl Pts',(-2.3747901511292,0.00119133359606537,
8.84858989190503));
#62077=CARTESIAN_POINT('Origin',(0.,0.,-1.84858989190501));
#62078=CARTESIAN_POINT('',(-2.37396076251026,0.0016408096299993,6.65141010809499));
#62079=CARTESIAN_POINT('',(-2.36824488832617,0.00085307042009708,6.84858989190503));
#62080=CARTESIAN_POINT('',(-2.37175,-2.62313128856983E-13,-1.84858989190501));
#62081=CARTESIAN_POINT('Ctrl Pts',(-2.37396076251026,0.00164080962999946,
6.65141010809499));
#62082=CARTESIAN_POINT('Ctrl Pts',(-2.36860111288507,-0.675161988858878,
6.69694933132258));
#62083=CARTESIAN_POINT('Ctrl Pts',(-1.71220786555833,-2.14309654094568,
6.79510892492056));
#62084=CARTESIAN_POINT('Ctrl Pts',(0.771789132562049,-2.68935864031417,
6.94588888888888));
#62085=CARTESIAN_POINT('Ctrl Pts',(2.67339522049833,-0.825388609316905,
7.10375));
#62086=CARTESIAN_POINT('Ctrl Pts',(2.15357369271338,1.7861771220756,7.26161111111111));
#62087=CARTESIAN_POINT('Ctrl Pts',(-0.3168471224657,2.77991299546561,7.41947222222222));
#62088=CARTESIAN_POINT('Ctrl Pts',(-2.11399942046796,1.52539245310181,7.54940522121685));
#62089=CARTESIAN_POINT('Ctrl Pts',(-2.36856127073871,0.369714310321545,
7.62671784984111));
#62090=CARTESIAN_POINT('Ctrl Pts',(-2.36801892187683,0.000385579322849869,
7.65141010809499));
#62091=CARTESIAN_POINT('Ctrl Pts',(-2.36824488832617,0.000853070420097184,
6.84858989190503));
#62092=CARTESIAN_POINT('Ctrl Pts',(-2.36678180876479,-0.447463537758943,
6.87857025960238));
#62093=CARTESIAN_POINT('Ctrl Pts',(-2.02943011823198,-1.68535627820218,
6.96121559096642));
#62094=CARTESIAN_POINT('Ctrl Pts',(-0.0362940343214689,-2.79846637663312,
7.09652588599712));
#62095=CARTESIAN_POINT('Ctrl Pts',(2.32391314315961,-1.55953807940794,7.2545207769972));
#62096=CARTESIAN_POINT('Ctrl Pts',(2.57596499873257,1.09413693995685,7.41251566799723));
#62097=CARTESIAN_POINT('Ctrl Pts',(0.491210792034311,2.75525738831465,7.5705105589973));
#62098=CARTESIAN_POINT('Ctrl Pts',(-1.83676464589149,1.98397717256952,7.71586863363322));
#62099=CARTESIAN_POINT('Ctrl Pts',(-2.36622439910258,0.594323617306658,
7.80856174460247));
#62100=CARTESIAN_POINT('Ctrl Pts',(-2.37158591103805,-0.002113965830532,
7.84858989190503));
#62101=CARTESIAN_POINT('Origin',(0.,0.,-1.84858989190501));
#62102=CARTESIAN_POINT('',(-2.37251499866524,-0.00203510706959473,5.65141010809499));
#62103=CARTESIAN_POINT('',(-2.37459246787895,0.00132584644941116,5.84858989190502));
#62104=CARTESIAN_POINT('',(-2.37175,-2.62313128856983E-13,-1.84858989190501));
#62105=CARTESIAN_POINT('Ctrl Pts',(-2.37251499866524,-0.00203510706959476,
5.65141010809499));
#62106=CARTESIAN_POINT('Ctrl Pts',(-2.37392982983489,-0.158778764602934,
5.66194007206332));
#62107=CARTESIAN_POINT('Ctrl Pts',(-2.28863365792017,-1.09727074999648,
5.72509040640203));
#62108=CARTESIAN_POINT('Ctrl Pts',(-1.03894725747156,-2.59786392206505,
5.84086111111111));
#62109=CARTESIAN_POINT('Ctrl Pts',(1.60611030100396,-2.29100808867664,5.99872222222222));
#62110=CARTESIAN_POINT('Ctrl Pts',(2.79643351757374,0.090928230838667,6.15658333333333));
#62111=CARTESIAN_POINT('Ctrl Pts',(1.45388718569001,2.39050630885174,6.31444444444444));
#62112=CARTESIAN_POINT('Ctrl Pts',(-1.20551740739643,2.52488339173069,6.47230555555556));
#62113=CARTESIAN_POINT('Ctrl Pts',(-2.3208356274226,0.99330351170231,6.58462744343907));
#62114=CARTESIAN_POINT('Ctrl Pts',(-2.37479416424485,0.106880641648857,
6.64432896095221));
#62115=CARTESIAN_POINT('Ctrl Pts',(-2.37396076251026,0.00164080962999946,
6.65141010809499));
#62116=CARTESIAN_POINT('Ctrl Pts',(-2.37459246787895,0.00132584644941126,
5.84858989190502));
#62117=CARTESIAN_POINT('Ctrl Pts',(-2.3698592307678,-0.701510136856058,
5.8959138109356));
#62118=CARTESIAN_POINT('Ctrl Pts',(-1.6684907359976,-2.19471791424095,5.99590269363287));
#62119=CARTESIAN_POINT('Ctrl Pts',(0.864288593995119,-2.66190468356086,
6.14855653999681));
#62120=CARTESIAN_POINT('Ctrl Pts',(2.70163876039796,-0.730670463607777,
6.30655143099686));
#62121=CARTESIAN_POINT('Ctrl Pts',(2.08817696449889,1.86339697407977,6.46454632199692));
#62122=CARTESIAN_POINT('Ctrl Pts',(-0.419590302218696,2.76706980330411,
6.62254121299697));
#62123=CARTESIAN_POINT('Ctrl Pts',(-2.14308835195883,1.46541542002878,6.75055573629967));
#62124=CARTESIAN_POINT('Ctrl Pts',(-2.36935192507288,0.340071095547311,
6.82590529593569));
#62125=CARTESIAN_POINT('Ctrl Pts',(-2.36824488832617,0.000853070420097184,
6.84858989190503));
#62126=CARTESIAN_POINT('Origin',(0.,0.,-1.84858989190501));
#62127=CARTESIAN_POINT('',(-2.36803551809634,0.000435659979227324,4.65141010809499));
#62128=CARTESIAN_POINT('',(-2.37186713520955,-0.00210673407030348,4.84858989190502));
#62129=CARTESIAN_POINT('',(-2.37175,-2.62313128856983E-13,-1.84858989190501));
#62130=CARTESIAN_POINT('Ctrl Pts',(-2.36803551809634,0.000435659979227676,
4.65141010809499));
#62131=CARTESIAN_POINT('Ctrl Pts',(-2.36733685507668,-0.420470574046625,
4.67955118317444));
#62132=CARTESIAN_POINT('Ctrl Pts',(-2.06020439223756,-1.62937224150312,
4.76031262862425));
#62133=CARTESIAN_POINT('Ctrl Pts',(-0.135586668767159,-2.79462423533096,
4.89369444444444));
#62134=CARTESIAN_POINT('Ctrl Pts',(2.2650598786042,-1.64250178316317,5.05155555555556));
#62135=CARTESIAN_POINT('Ctrl Pts',(2.61412853009539,0.997316594419356,5.20941666666666));
#62136=CARTESIAN_POINT('Ctrl Pts',(0.595450368366912,2.73381550588105,5.36727777777778));
#62137=CARTESIAN_POINT('Ctrl Pts',(-1.79192767962886,2.0434990191552,5.51460892492054));
#62138=CARTESIAN_POINT('Ctrl Pts',(-2.36685963088812,0.624501153297232,
5.60931970169295));
#62139=CARTESIAN_POINT('Ctrl Pts',(-2.37251499866524,-0.00203510706959476,
5.65141010809499));
#62140=CARTESIAN_POINT('Ctrl Pts',(-2.37186713520955,-0.00210673407030307,
4.84858989190502));
#62141=CARTESIAN_POINT('Ctrl Pts',(-2.37348726775032,-0.180895246540068,
4.86059239860214));
#62142=CARTESIAN_POINT('Ctrl Pts',(-2.27367886126175,-1.14238681798702,
4.92525986896595));
#62143=CARTESIAN_POINT('Ctrl Pts',(-0.964512940920624,-2.62725067416123,
5.04259230299644));
#62144=CARTESIAN_POINT('Ctrl Pts',(1.67331967629405,-2.24337526486265,5.20058719399648));
#62145=CARTESIAN_POINT('Ctrl Pts',(2.79318773824162,0.175594923072764,5.35858208499656));
#62146=CARTESIAN_POINT('Ctrl Pts',(1.37919449268132,2.43527285317938,5.51657697599659));
#62147=CARTESIAN_POINT('Ctrl Pts',(-1.28594543116668,2.48577466117395,5.67457186699666));
#62148=CARTESIAN_POINT('Ctrl Pts',(-2.33566190719347,0.94159330950118,5.78524283896613));
#62149=CARTESIAN_POINT('Ctrl Pts',(-2.37512666773395,0.0806489125773547,
5.84324884726892));
#62150=CARTESIAN_POINT('Ctrl Pts',(-2.37459246787895,0.00132584644941126,
5.84858989190502));
#62151=CARTESIAN_POINT('Origin',(0.,0.,-1.84858989190501));
#62152=CARTESIAN_POINT('',(-2.37404189208837,0.00160568163382189,3.65141010809499));
#62153=CARTESIAN_POINT('',(-2.36815046112586,0.00071106261527204,3.84858989190502));
#62154=CARTESIAN_POINT('',(-2.37175,-2.62313128856983E-13,-1.84858989190501));
#62155=CARTESIAN_POINT('Ctrl Pts',(-2.37404189208837,0.0016056816338219,
3.65141010809499));
#62156=CARTESIAN_POINT('Ctrl Pts',(-2.36874097406567,-0.678301390146093,
3.69716229428555));
#62157=CARTESIAN_POINT('Ctrl Pts',(-1.70710264047504,-2.14919504149034,
3.79553485084648));
#62158=CARTESIAN_POINT('Ctrl Pts',(0.782578662553965,-2.68623882063674,
3.94652777777777));
#62159=CARTESIAN_POINT('Ctrl Pts',(2.67668699402767,-0.814650291328897,
4.10438888888889));
#62160=CARTESIAN_POINT('Ctrl Pts',(2.14638618582228,1.79480770611467,4.26225));
#62161=CARTESIAN_POINT('Ctrl Pts',(-0.328003825581952,2.77861869501174,
4.42011111111111));
#62162=CARTESIAN_POINT('Ctrl Pts',(-2.1171683957745,1.51896204170615,4.54983114714277));
#62163=CARTESIAN_POINT('Ctrl Pts',(-2.3686432695173,0.366572631058683,4.62693081280407));
#62164=CARTESIAN_POINT('Ctrl Pts',(-2.36803551809634,0.000435659979227676,
4.65141010809499));
#62165=CARTESIAN_POINT('Ctrl Pts',(-2.36815046112586,0.000711062615271901,
3.84858989190502));
#62166=CARTESIAN_POINT('Ctrl Pts',(-2.36695951468436,-0.438164069114789,
3.87793594993537));
#62167=CARTESIAN_POINT('Ctrl Pts',(-2.04015506879268,-1.66630099353556,
3.9599469716324));
#62168=CARTESIAN_POINT('Ctrl Pts',(-0.0697503817448946,-2.79783241149437,
4.09462295699612));
#62169=CARTESIAN_POINT('Ctrl Pts',(2.30510093209087,-1.58721170953314,4.25261784799616));
#62170=CARTESIAN_POINT('Ctrl Pts',(2.5888625630092,1.06326005653742,4.41061273899623));
#62171=CARTESIAN_POINT('Ctrl Pts',(0.524118009051023,2.74918744918107,4.56860762999628));
#62172=CARTESIAN_POINT('Ctrl Pts',(-1.82311086019465,2.00255204277458,4.71460001429921));
#62173=CARTESIAN_POINT('Ctrl Pts',(-2.36637840094874,0.603598422228309,
4.80792743493546));
#62174=CARTESIAN_POINT('Ctrl Pts',(-2.37186713520955,-0.00210673407030307,
4.84858989190502));
#62175=CARTESIAN_POINT('Origin',(0.,0.,-1.84858989190501));
#62176=CARTESIAN_POINT('',(-2.37242086931256,-0.00204814969984112,2.65141010809499));
#62177=CARTESIAN_POINT('',(-2.37437841508221,0.00145143062880153,2.84858989190502));
#62178=CARTESIAN_POINT('',(-2.37175,-2.62313128856983E-13,-1.84858989190501));
#62179=CARTESIAN_POINT('Ctrl Pts',(-2.37242086931256,-0.00204814969984169,
2.65141010809499));
#62180=CARTESIAN_POINT('Ctrl Pts',(-2.37386724785776,-0.161978223542019,
2.66215303502629));
#62181=CARTESIAN_POINT('Ctrl Pts',(-2.28652040521148,-1.10369798895945,
2.72551633232796));
#62182=CARTESIAN_POINT('Ctrl Pts',(-1.02851040967351,-2.60201352259292,
2.84149999999999));
#62183=CARTESIAN_POINT('Ctrl Pts',(1.61529402596567,-2.28454233775194,2.99936111111111));
#62184=CARTESIAN_POINT('Ctrl Pts',(2.79604598097933,0.102153087721166,3.15722222222222));
#62185=CARTESIAN_POINT('Ctrl Pts',(1.44427938842878,2.39632330140064,3.31508333333333));
#62186=CARTESIAN_POINT('Ctrl Pts',(-1.21564319790733,2.5200238088076,3.47294444444445));
#62187=CARTESIAN_POINT('Ctrl Pts',(-2.32270131739363,0.986891451715146,
3.58505336936499));
#62188=CARTESIAN_POINT('Ctrl Pts',(-2.37483765037521,0.103671339757588,
3.64454192391517));
#62189=CARTESIAN_POINT('Ctrl Pts',(-2.37404189208837,0.0016056816338219,
3.65141010809499));
#62190=CARTESIAN_POINT('Ctrl Pts',(-2.37437841508221,0.00145143062880148,
2.84858989190502));
#62191=CARTESIAN_POINT('Ctrl Pts',(-2.36936657242201,-0.69212851464997,
2.89527950126859));
#62192=CARTESIAN_POINT('Ctrl Pts',(-1.68411161328175,-2.17667922631145,
2.99463407429885));
#62193=CARTESIAN_POINT('Ctrl Pts',(0.832400628534772,-2.67204800324426,
3.1466536109958));
#62194=CARTESIAN_POINT('Ctrl Pts',(2.69270963387839,-0.762919488957052,
3.30464850199585));
#62195=CARTESIAN_POINT('Ctrl Pts',(2.11030679852043,1.83829718168443,3.4626433929959));
#62196=CARTESIAN_POINT('Ctrl Pts',(-0.386476751895552,2.77188871376435,
3.62063828399595));
#62197=CARTESIAN_POINT('Ctrl Pts',(-2.13403081733917,1.48458669705641,3.74928711696566));
#62198=CARTESIAN_POINT('Ctrl Pts',(-2.36909680859298,0.349449137499666,
3.82527098626868));
#62199=CARTESIAN_POINT('Ctrl Pts',(-2.36815046112586,0.000711062615271901,
3.84858989190502));
#62200=CARTESIAN_POINT('Origin',(0.,0.,-1.84858989190501));
#62201=CARTESIAN_POINT('',(-2.36805372255214,0.000487775483918624,1.65141010809499));
#62202=CARTESIAN_POINT('',(-2.37214954248261,-0.00208751672060303,1.84858989190502));
#62203=CARTESIAN_POINT('',(-2.37175,-2.62313128856983E-13,-1.84858989190501));
#62204=CARTESIAN_POINT('Ctrl Pts',(-2.36805372255214,0.000487775483918769,
1.65141010809499));
#62205=CARTESIAN_POINT('Ctrl Pts',(-2.36726911244657,-0.423596588857836,
1.6797641461374));
#62206=CARTESIAN_POINT('Ctrl Pts',(-2.0567282222087,-1.63578530702029,1.76073855455018));
#62207=CARTESIAN_POINT('Ctrl Pts',(-0.124366744542119,-2.79514315034066,
1.89433333333333));
#62208=CARTESIAN_POINT('Ctrl Pts',(2.27163476293377,-1.63339753074864,2.05219444444444));
#62209=CARTESIAN_POINT('Ctrl Pts',(2.61010413592219,1.00780309522069,2.21005555555555));
#62210=CARTESIAN_POINT('Ctrl Pts',(0.584471286669745,2.73618335546233,2.36791666666667));
#62211=CARTESIAN_POINT('Ctrl Pts',(-1.79666946585791,2.03730116384381,2.51503485084647));
#62212=CARTESIAN_POINT('Ctrl Pts',(-2.36678268187025,0.621381820955435,
2.60953266465592));
#62213=CARTESIAN_POINT('Ctrl Pts',(-2.37242086931256,-0.00204814969984169,
2.65141010809499));
#62214=CARTESIAN_POINT('Ctrl Pts',(-2.37214954248261,-0.00208751672060286,
1.84858989190502));
#62215=CARTESIAN_POINT('Ctrl Pts',(-2.37368814589582,-0.171375740131997,
1.85995808893514));
#62216=CARTESIAN_POINT('Ctrl Pts',(-2.28019409230745,-1.12323247312203,
1.92399124963194));
#62217=CARTESIAN_POINT('Ctrl Pts',(-0.995855715555496,-2.61553061219188,
2.04068937399542));
#62218=CARTESIAN_POINT('Ctrl Pts',(1.64637781974439,-2.26322161422709,2.19868426499547));
#62219=CARTESIAN_POINT('Ctrl Pts',(2.79508756969503,0.142186649832604,2.35667915599553));
#62220=CARTESIAN_POINT('Ctrl Pts',(1.40821242874264,2.41860884498944,2.51467404699558));
#62221=CARTESIAN_POINT('Ctrl Pts',(-1.25613315819632,2.50097199645567,2.67266893799564));
#62222=CARTESIAN_POINT('Ctrl Pts',(-2.33035893824447,0.960673681793537,
2.78397421963211));
#62223=CARTESIAN_POINT('Ctrl Pts',(-2.37501983264844,0.0902160608552179,
2.84261453760191));
#62224=CARTESIAN_POINT('Ctrl Pts',(-2.37437841508221,0.00145143062880148,
2.84858989190502));
#62225=CARTESIAN_POINT('Origin',(0.,0.,-1.84858989190501));
#62226=CARTESIAN_POINT('',(-2.37409249406917,0.00172857025301859,0.651410108094985));
#62227=CARTESIAN_POINT('',(-2.36806791026422,0.000580996437929415,0.848589891905023));
#62228=CARTESIAN_POINT('',(-2.37175,-2.62313128856983E-13,-1.84858989190501));
#62229=CARTESIAN_POINT('Ctrl Pts',(-2.37409249406917,0.00172857025301858,
0.651410108094986));
#62230=CARTESIAN_POINT('Ctrl Pts',(-2.36885059157359,-0.681255271864669,
0.697375257248508));
#62231=CARTESIAN_POINT('Ctrl Pts',(-1.70202128243095,-2.15553453151225,
0.7959607767724));
#62232=CARTESIAN_POINT('Ctrl Pts',(0.793380919254056,-2.68293732976497,
0.947166666666663));
#62233=CARTESIAN_POINT('Ctrl Pts',(2.67992237177449,-0.803971281251394,
1.10502777777777));
#62234=CARTESIAN_POINT('Ctrl Pts',(2.13917103413275,1.80344728451176,1.26288888888888));
#62235=CARTESIAN_POINT('Ctrl Pts',(-0.339158877291603,2.77725977180218,
1.42075));
#62236=CARTESIAN_POINT('Ctrl Pts',(-2.12031894951391,1.51253569372851,1.5502570730687));
#62237=CARTESIAN_POINT('Ctrl Pts',(-2.36872521807391,0.363433332120877,
1.62714377576703));
#62238=CARTESIAN_POINT('Ctrl Pts',(-2.36805372255214,0.000487775483918769,
1.65141010809499));
#62239=CARTESIAN_POINT('Ctrl Pts',(-2.36806791026422,0.000580996437929554,
0.848589891905023));
#62240=CARTESIAN_POINT('Ctrl Pts',(-2.36714590954407,-0.428850691797627,
0.877301640268363));
#62241=CARTESIAN_POINT('Ctrl Pts',(-2.05072593975983,-1.64725737587436,
0.958678352298389));
#62242=CARTESIAN_POINT('Ctrl Pts',(-0.103189861818606,-2.79677945469355,
1.0927200279951));
#62243=CARTESIAN_POINT('Ctrl Pts',(2.28595558559378,-1.6146683983646,1.25071491899515));
#62244=CARTESIAN_POINT('Ctrl Pts',(2.60139192527736,1.0322363870214,1.4087098099952));
#62245=CARTESIAN_POINT('Ctrl Pts',(0.556949311928898,2.7427217714679,1.56670470099526));
#62246=CARTESIAN_POINT('Ctrl Pts',(-1.80927361374524,2.02108563130788,1.7133313949652));
#62247=CARTESIAN_POINT('Ctrl Pts',(-2.36656032319539,0.612878624174093,
1.80729312526845));
#62248=CARTESIAN_POINT('Ctrl Pts',(-2.37214954248261,-0.00208751672060286,
1.84858989190502));
#62249=CARTESIAN_POINT('Origin',(0.,0.,15.5));
#62250=CARTESIAN_POINT('',(-2.86987326377042,0.00104132824445593,15.1339652973708));
#62251=CARTESIAN_POINT('Ctrl Pts',(-0.439445221994174,2.33068358199188,
15.62825));
#62252=CARTESIAN_POINT('Ctrl Pts',(-0.359491362851287,2.34930954683752,
15.6247606402091));
#62253=CARTESIAN_POINT('Ctrl Pts',(-0.27873128971825,2.36341107797762,15.6212855109979));
#62254=CARTESIAN_POINT('Ctrl Pts',(-0.197490043658781,2.37317361481181,
15.6178198845782));
#62255=CARTESIAN_POINT('Ctrl Pts',(-0.114097433923979,2.38319467509491,
15.6142624842978));
#62256=CARTESIAN_POINT('Ctrl Pts',(-0.0301970746788968,2.38864392614809,
15.610715096763));
#62257=CARTESIAN_POINT('Ctrl Pts',(0.0538748377108959,2.38966967391038,
15.6071726085593));
#62258=CARTESIAN_POINT('Ctrl Pts',(0.0936167287327529,2.39015455827456,
15.6054980281181));
#62259=CARTESIAN_POINT('Ctrl Pts',(0.133397101437596,2.38965022998153,15.6038245424699));
#62260=CARTESIAN_POINT('Ctrl Pts',(0.17318082101162,2.38816842541213,15.6021516114778));
#62261=CARTESIAN_POINT('Ctrl Pts',(0.19744268730314,2.38726475565179,15.601131384398));
#62262=CARTESIAN_POINT('Ctrl Pts',(0.221705799792773,2.38599750448324,15.6001113636003));
#62263=CARTESIAN_POINT('Ctrl Pts',(0.245962166148401,2.38436888753973,15.5990914265778));
#62264=CARTESIAN_POINT('Ctrl Pts',(0.26185491634123,2.38330181913124,15.5984231647255));
#62265=CARTESIAN_POINT('Ctrl Pts',(0.277745619245824,2.38207945021967,15.597754902985));
#62266=CARTESIAN_POINT('Ctrl Pts',(0.293615508622687,2.38070402970992,15.5970873017022));
#62267=CARTESIAN_POINT('Ctrl Pts',(0.379355905904818,2.37327303267301,15.5934804461119));
#62268=CARTESIAN_POINT('Ctrl Pts',(0.46460122999168,2.36137220783444,15.5898881158652));
#62269=CARTESIAN_POINT('Ctrl Pts',(0.548999070996607,2.3451645872232,15.5863050764217));
#62270=CARTESIAN_POINT('Ctrl Pts',(0.634137600151781,2.32881472609505,15.582690591685));
#62271=CARTESIAN_POINT('Ctrl Pts',(0.718414656351904,2.30808199543454,15.5790855615419));
#62272=CARTESIAN_POINT('Ctrl Pts',(0.801467682213623,2.28308069981211,15.5754846124216));
#62273=CARTESIAN_POINT('Ctrl Pts',(0.852459500288906,2.26773072905791,15.573273748452));
#62274=CARTESIAN_POINT('Ctrl Pts',(0.902989840792886,2.2507706713731,15.5710644228464));
#62275=CARTESIAN_POINT('Ctrl Pts',(0.952972256247749,2.23221757070223,15.5688553919549));
#62276=CARTESIAN_POINT('Ctrl Pts',(0.964785636442244,2.22783253188374,15.5683332858993));
#62277=CARTESIAN_POINT('Ctrl Pts',(0.976567164733754,2.22335887755768,15.5678112499871));
#62278=CARTESIAN_POINT('Ctrl Pts',(0.98830665315667,2.21880049805757,15.5672896716409));
#62279=CARTESIAN_POINT('Ctrl Pts',(1.07009362440554,2.18704306198486,15.5636559261431));
#62280=CARTESIAN_POINT('Ctrl Pts',(1.14996182974845,2.15113305037133,15.5600390318413));
#62281=CARTESIAN_POINT('Ctrl Pts',(1.22755227573139,2.11121890826833,15.5564336755567));
#62282=CARTESIAN_POINT('Ctrl Pts',(1.30476387614222,2.07149965222131,15.552845922899));
#62283=CARTESIAN_POINT('Ctrl Pts',(1.37972085381243,2.02781498993708,15.5492695958616));
#62284=CARTESIAN_POINT('Ctrl Pts',(1.45205674723287,1.98026157738062,15.5456994587133));
#62285=CARTESIAN_POINT('Ctrl Pts',(1.51163119176407,1.94109750537355,15.5427591627211));
#62286=CARTESIAN_POINT('Ctrl Pts',(1.56942781249227,1.89930836286272,15.5398230652386));
#62287=CARTESIAN_POINT('Ctrl Pts',(1.62522850219512,1.85492460083693,15.5368882414682));
#62288=CARTESIAN_POINT('Ctrl Pts',(1.65312884704655,1.83273271982404,15.5354208295831));
#62289=CARTESIAN_POINT('Ctrl Pts',(1.68052998038672,1.80989186082895,15.5339537361259));
#62290=CARTESIAN_POINT('Ctrl Pts',(1.70740302888556,1.78640394209333,15.532486595497));
#62291=CARTESIAN_POINT('Ctrl Pts',(1.72592667853778,1.77021366960761,15.5314752923321));
#62292=CARTESIAN_POINT('Ctrl Pts',(1.74419939199006,1.753715928893,15.5304639667541));
#62293=CARTESIAN_POINT('Ctrl Pts',(1.76221135665739,1.73691101229318,15.5294524990243));
#62294=CARTESIAN_POINT('Ctrl Pts',(1.77033011726031,1.72933631972932,15.528996587384));
#62295=CARTESIAN_POINT('Ctrl Pts',(1.77839409985328,1.72170084478485,15.5285407465195));
#62296=CARTESIAN_POINT('Ctrl Pts',(1.78639747681482,1.71400960641012,15.5280852527741));
#62297=CARTESIAN_POINT('Ctrl Pts',(1.84657495109044,1.65617910540199,15.5246603905846));
#62298=CARTESIAN_POINT('Ctrl Pts',(1.90341295390484,1.59512114682347,15.5212504095826));
#62299=CARTESIAN_POINT('Ctrl Pts',(1.95689046613085,1.53122773141625,15.5178508639384));
#62300=CARTESIAN_POINT('Ctrl Pts',(2.01194103421405,1.46545487347031,15.5143513197161));
#62301=CARTESIAN_POINT('Ctrl Pts',(2.06343093897923,1.39667671283205,15.5108628337987));
#62302=CARTESIAN_POINT('Ctrl Pts',(2.11130423046702,1.3252770563036,15.507380556377));
#62303=CARTESIAN_POINT('Ctrl Pts',(2.15745742078722,1.25644281002257,15.5040233981871));
#62304=CARTESIAN_POINT('Ctrl Pts',(2.20024928268006,1.18517117106803,15.500672010362));
#62305=CARTESIAN_POINT('Ctrl Pts',(2.23959635988792,1.11177753196584,15.4973220472993));
#62306=CARTESIAN_POINT('Ctrl Pts',(2.25681070616636,1.07966781485864,15.4958564384594));
#62307=CARTESIAN_POINT('Ctrl Pts',(2.27336525378777,1.04715163497876,15.4943911023279));
#62308=CARTESIAN_POINT('Ctrl Pts',(2.28925084670373,1.0142542353915,15.4929256750031));
#62309=CARTESIAN_POINT('Ctrl Pts',(2.29885484868501,0.994365352899876,15.4920397170785));
#62310=CARTESIAN_POINT('Ctrl Pts',(2.30821431569525,0.974337119524171,15.491153725822));
#62311=CARTESIAN_POINT('Ctrl Pts',(2.3173269757796,0.954175024263046,15.4902676208197));
#62312=CARTESIAN_POINT('Ctrl Pts',(2.32227232757467,0.943233251710468,15.4897867402729));
#62313=CARTESIAN_POINT('Ctrl Pts',(2.32714420559321,0.932253683866113,15.4893058986854));
#62314=CARTESIAN_POINT('Ctrl Pts',(2.33193873109372,0.921245710398884,15.4888254510349));
#62315=CARTESIAN_POINT('Ctrl Pts',(2.36754247444614,0.839501424730483,15.4852576871677));
#62316=CARTESIAN_POINT('Ctrl Pts',(2.39894281260828,0.756064329075142,15.4817059560376));
#62317=CARTESIAN_POINT('Ctrl Pts',(2.42608268559146,0.671340103595013,15.4781652340513));
#62318=CARTESIAN_POINT('Ctrl Pts',(2.453534139292,0.58564319725637,15.4745838626229));
#62319=CARTESIAN_POINT('Ctrl Pts',(2.47662715562456,0.498628540954889,15.4710137545713));
#62320=CARTESIAN_POINT('Ctrl Pts',(2.49525785992387,0.410687466692489,15.4674497112883));
#62321=CARTESIAN_POINT('Ctrl Pts',(2.51258257274376,0.328910963121187,15.4641355034428));
#62322=CARTESIAN_POINT('Ctrl Pts',(2.52604844140045,0.24633247953868,15.4608265399003));
#62323=CARTESIAN_POINT('Ctrl Pts',(2.53553303361489,0.163255416668028,15.4575186404574));
#62324=CARTESIAN_POINT('Ctrl Pts',(2.53942998139287,0.129121426694033,15.4561595191486));
#62325=CARTESIAN_POINT('Ctrl Pts',(2.54265436806282,0.0949032017028567,
15.4548005774761));
#62326=CARTESIAN_POINT('Ctrl Pts',(2.54519570834653,0.0606216731012661,
15.4534415254952));
#62327=CARTESIAN_POINT('Ctrl Pts',(2.54650804671318,0.0429188233335401,
15.4527397162695));
#62328=CARTESIAN_POINT('Ctrl Pts',(2.5476382209856,0.0251990932110098,15.4520378776284));
#62329=CARTESIAN_POINT('Ctrl Pts',(2.54858465973821,0.00746537430393359,
15.4513359696452));
#62330=CARTESIAN_POINT('Ctrl Pts',(2.54936740774304,-0.00720121986763361,
15.4507554597369));
#62331=CARTESIAN_POINT('Ctrl Pts',(2.55002444266908,-0.0218786230829287,
15.4501748534934));
#62332=CARTESIAN_POINT('Ctrl Pts',(2.55055443165925,-0.0365475000712079,
15.4495948274855));
#62333=CARTESIAN_POINT('Ctrl Pts',(2.55387898415761,-0.128563471239416,
15.4459563992365));
#62334=CARTESIAN_POINT('Ctrl Pts',(2.55221836548087,-0.22040066645441,15.4423345418383));
#62335=CARTESIAN_POINT('Ctrl Pts',(2.5454697064449,-0.311650010793409,15.4387239299593));
#62336=CARTESIAN_POINT('Ctrl Pts',(2.53872104740894,-0.402899355132408,
15.4351133180804));
#62337=CARTESIAN_POINT('Ctrl Pts',(2.52688470709894,-0.49356189746232,15.4315139517205));
#62338=CARTESIAN_POINT('Ctrl Pts',(2.50980235603637,-0.583236219097685,
15.4279205055482));
#62339=CARTESIAN_POINT('Ctrl Pts',(2.49326213150481,-0.670064631014266,
15.424441101202));
#62340=CARTESIAN_POINT('Ctrl Pts',(2.47180332144007,-0.755967381987536,
15.420967247239));
#62341=CARTESIAN_POINT('Ctrl Pts',(2.44569482135312,-0.840684658565203,
15.4174941094224));
#62342=CARTESIAN_POINT('Ctrl Pts',(2.43658807165331,-0.870234384917672,
15.4162826650015));
#62343=CARTESIAN_POINT('Ctrl Pts',(2.42691516765274,-0.899639766052948,
15.41507130771));
#62344=CARTESIAN_POINT('Ctrl Pts',(2.41668612527745,-0.928889320342703,
15.4138598323975));
#62345=CARTESIAN_POINT('Ctrl Pts',(2.41079789512425,-0.945726488595391,
15.4131624606198));
#62346=CARTESIAN_POINT('Ctrl Pts',(2.40472537046329,-0.962512016907764,
15.4124650497348));
#62347=CARTESIAN_POINT('Ctrl Pts',(2.39847036187175,-0.979243667871416,
15.4117675606113));
#62348=CARTESIAN_POINT('Ctrl Pts',(2.39421301098727,-0.990631743201221,
15.4112928281));
#62349=CARTESIAN_POINT('Ctrl Pts',(2.38987156242605,-1.0019935463669,15.4108181134517));
#62350=CARTESIAN_POINT('Ctrl Pts',(2.38545028303317,-1.01331939423191,15.4103437824454));
#62351=CARTESIAN_POINT('Ctrl Pts',(2.35279097735238,-1.09698167717045,15.4068399728119));
#62352=CARTESIAN_POINT('Ctrl Pts',(2.31572987674733,-1.17881857921774,15.4033514296728));
#62353=CARTESIAN_POINT('Ctrl Pts',(2.27459874133947,-1.25857844945699,15.3998733992833));
#62354=CARTESIAN_POINT('Ctrl Pts',(2.23281288372258,-1.33960793109688,15.396340005877));
#62355=CARTESIAN_POINT('Ctrl Pts',(2.18682594253521,-1.41849449977561,15.3928174625663));
#62356=CARTESIAN_POINT('Ctrl Pts',(2.13693151879332,-1.49496175096055,15.3893007849646));
#62357=CARTESIAN_POINT('Ctrl Pts',(2.08679723793274,-1.57179660263405,15.385767201663));
#62358=CARTESIAN_POINT('Ctrl Pts',(2.03271725897117,-1.64618961960946,15.3822395406022));
#62359=CARTESIAN_POINT('Ctrl Pts',(1.97494281786374,-1.71783598585985,15.3787127451654));
#62360=CARTESIAN_POINT('Ctrl Pts',(1.95216878512211,-1.74607817495815,15.3773225222016));
#62361=CARTESIAN_POINT('Ctrl Pts',(1.92882022676702,-1.77389324483966,15.3759324337425));
#62362=CARTESIAN_POINT('Ctrl Pts',(1.90491084697345,-1.80126106485015,15.3745421700657));
#62363=CARTESIAN_POINT('Ctrl Pts',(1.89303589564547,-1.8148537022746,15.3738516748025));
#62364=CARTESIAN_POINT('Ctrl Pts',(1.88102258946071,-1.82833599951471,15.3731611363172));
#62365=CARTESIAN_POINT('Ctrl Pts',(1.86887253021617,-1.84170540057035,15.3724705166642));
#62366=CARTESIAN_POINT('Ctrl Pts',(1.86055716973053,-1.85085526453538,15.3719978645349));
#62367=CARTESIAN_POINT('Ctrl Pts',(1.8521789913077,-1.85995082597714,15.3715252464369));
#62368=CARTESIAN_POINT('Ctrl Pts',(1.84374494253208,-1.86898463564396,15.3710530027583));
#62369=CARTESIAN_POINT('Ctrl Pts',(1.77862481272331,-1.93873557897155,15.3674067623267));
#62370=CARTESIAN_POINT('Ctrl Pts',(1.71007452953627,-2.00492197279666,15.3637769310107));
#62371=CARTESIAN_POINT('Ctrl Pts',(1.63841756617314,-2.06724394639147,15.3601581531957));
#62372=CARTESIAN_POINT('Ctrl Pts',(1.56864469297252,-2.1279272764847,15.3566345245939));
#62373=CARTESIAN_POINT('Ctrl Pts',(1.49592552744324,-2.18494739655425,15.3531213758712));
#62374=CARTESIAN_POINT('Ctrl Pts',(1.42051657448793,-2.237996979208,15.3496137628515));
#62375=CARTESIAN_POINT('Ctrl Pts',(1.34626553575621,-2.29023197866037,15.3461600096832));
#62376=CARTESIAN_POINT('Ctrl Pts',(1.26940602418092,-2.33861808827242,15.3427116235202));
#62377=CARTESIAN_POINT('Ctrl Pts',(1.19015227451303,-2.38282228508801,15.3392638844625));
#62378=CARTESIAN_POINT('Ctrl Pts',(1.16438136391748,-2.39719614637352,15.3381427845096));
#62379=CARTESIAN_POINT('Ctrl Pts',(1.1383570943619,-2.4111274748391,15.3370217529787));
#62380=CARTESIAN_POINT('Ctrl Pts',(1.11208629310672,-2.42460372067378,15.3359006275904));
#62381=CARTESIAN_POINT('Ctrl Pts',(1.09252404263768,-2.4346386523776,15.3350657944447));
#62382=CARTESIAN_POINT('Ctrl Pts',(1.07282508844486,-2.44442123549769,15.3342309092564));
#62383=CARTESIAN_POINT('Ctrl Pts',(1.05299217133848,-2.4539460706498,15.3333959050218));
#62384=CARTESIAN_POINT('Ctrl Pts',(1.04038456497523,-2.46000092237074,15.3328651003678));
#62385=CARTESIAN_POINT('Ctrl Pts',(1.02772285622574,-2.46595150778408,15.3323342505181));
#62386=CARTESIAN_POINT('Ctrl Pts',(1.01502087310116,-2.47179063085649,15.3318038822616));
#62387=CARTESIAN_POINT('Ctrl Pts',(0.982652722257195,-2.48667032440912,
15.3304523578927));
#62388=CARTESIAN_POINT('Ctrl Pts',(0.950002091670773,-2.50083650005249,
15.3291030741213));
#62389=CARTESIAN_POINT('Ctrl Pts',(0.917084170499721,-2.5142729570447,15.3277557583224));
#62390=CARTESIAN_POINT('Ctrl Pts',(0.834495683370104,-2.5479839757206,15.3243754484619));
#62391=CARTESIAN_POINT('Ctrl Pts',(0.750226663082229,-2.57710500546031,
15.3210075263739));
#62392=CARTESIAN_POINT('Ctrl Pts',(0.664646844355562,-2.60177034865307,
15.317647686521));
#62393=CARTESIAN_POINT('Ctrl Pts',(0.576787650214132,-2.6270926408521,15.3141983590239));
#62394=CARTESIAN_POINT('Ctrl Pts',(0.487546169865586,-2.64771888106776,
15.3107575500279));
#62395=CARTESIAN_POINT('Ctrl Pts',(0.397298853288816,-2.66374516605354,
15.3073206007236));
#62396=CARTESIAN_POINT('Ctrl Pts',(0.308910977458226,-2.67944124812091,
15.3039544657529));
#62397=CARTESIAN_POINT('Ctrl Pts',(0.219557440695963,-2.69072476824651,
15.3005920330634));
#62398=CARTESIAN_POINT('Ctrl Pts',(0.129581594551193,-2.69764046998944,
15.2972289259214));
#62399=CARTESIAN_POINT('Ctrl Pts',(0.0974227261046785,-2.7001122571645,
15.2960268953233));
#62400=CARTESIAN_POINT('Ctrl Pts',(0.0651843226484069,-2.70202565483482,
15.2948247785662));
#62401=CARTESIAN_POINT('Ctrl Pts',(0.0328820436324132,-2.7033813247538,
15.2936223758136));
#62402=CARTESIAN_POINT('Ctrl Pts',(0.0192199250543532,-2.70395469987624,
15.2931138244208));
#62403=CARTESIAN_POINT('Ctrl Pts',(0.00555605037576419,-2.70442788901379,
15.2926055817652));
#62404=CARTESIAN_POINT('Ctrl Pts',(-0.00810768527292701,-2.70480131817288,
15.2920976575977));
#62405=CARTESIAN_POINT('Ctrl Pts',(-0.102177189495074,-2.70737223265483,
15.2886007973064));
#62406=CARTESIAN_POINT('Ctrl Pts',(-0.196248953232544,-2.705219350857,15.2851186519246));
#62407=CARTESIAN_POINT('Ctrl Pts',(-0.28992790026966,-2.69846111693802,
15.2816464960614));
#62408=CARTESIAN_POINT('Ctrl Pts',(-0.384721183626751,-2.69162249200534,
15.2781330379685));
#62409=CARTESIAN_POINT('Ctrl Pts',(-0.479113197863739,-2.68006831395088,
15.2746298084638));
#62410=CARTESIAN_POINT('Ctrl Pts',(-0.572703609774366,-2.66386867615587,
15.2711319115131));
#62411=CARTESIAN_POINT('Ctrl Pts',(-0.670406973022026,-2.64695712438838,
15.2674802949704));
#62412=CARTESIAN_POINT('Ctrl Pts',(-0.767237930320469,-2.62498318167097,
15.2638344899723));
#62413=CARTESIAN_POINT('Ctrl Pts',(-0.862734200133818,-2.5979664405403,
15.2601889262148));
#62414=CARTESIAN_POINT('Ctrl Pts',(-0.899309423475345,-2.58761898568426,
15.258792669493));
#62415=CARTESIAN_POINT('Ctrl Pts',(-0.935688693950487,-2.57653116703875,
15.2573964481588));
#62416=CARTESIAN_POINT('Ctrl Pts',(-0.971845190453781,-2.56470173355219,
15.2559999492582));
#62417=CARTESIAN_POINT('Ctrl Pts',(-0.985718422450195,-2.56016278506391,
15.2554641132369));
#62418=CARTESIAN_POINT('Ctrl Pts',(-0.999558849945709,-2.55551463851664,
15.2549282363508));
#62419=CARTESIAN_POINT('Ctrl Pts',(-1.01336493152648,-2.55075717270086,
15.254392300921));
#62420=CARTESIAN_POINT('Ctrl Pts',(-1.02713823497804,-2.5460110019675,15.2538576378986));
#62421=CARTESIAN_POINT('Ctrl Pts',(-1.0408680078023,-2.54115923920241,15.2533232792799));
#62422=CARTESIAN_POINT('Ctrl Pts',(-1.05455083068562,-2.53620294641156,
15.2527892870021));
#62423=CARTESIAN_POINT('Ctrl Pts',(-1.14480706402235,-2.50350966941525,
15.2492669048126));
#62424=CARTESIAN_POINT('Ctrl Pts',(-1.23304972084596,-2.46626241239109,
15.2457593395817));
#62425=CARTESIAN_POINT('Ctrl Pts',(-1.3188786706842,-2.42453542284507,15.242261762893));
#62426=CARTESIAN_POINT('Ctrl Pts',(-1.40341018907482,-2.38343919842613,
15.238817057246));
#62427=CARTESIAN_POINT('Ctrl Pts',(-1.48560133565556,-2.33799743942912,
15.2353820404405));
#62428=CARTESIAN_POINT('Ctrl Pts',(-1.56505752288372,-2.28823266258407,
15.2319520997326));
#62429=CARTESIAN_POINT('Ctrl Pts',(-1.59875150777533,-2.26712954025155,
15.2304976079627));
#62430=CARTESIAN_POINT('Ctrl Pts',(-1.63195344745741,-2.24524844976825,
15.2290440290004));
#62431=CARTESIAN_POINT('Ctrl Pts',(-1.66463195977674,-2.22258855435451,
15.2275910110965));
#62432=CARTESIAN_POINT('Ctrl Pts',(-1.74176819837999,-2.16910083489293,
15.2241612241271));
#62433=CARTESIAN_POINT('Ctrl Pts',(-1.81599039866318,-2.11127647963352,
15.2207345632396));
#62434=CARTESIAN_POINT('Ctrl Pts',(-1.88715256813859,-2.04946422501414,
15.2173064022613));
#62435=CARTESIAN_POINT('Ctrl Pts',(-1.90164577925548,-2.03687526008497,
15.2166082074035));
#62436=CARTESIAN_POINT('Ctrl Pts',(-1.91601194648249,-2.02412075255685,
15.215909950323));
#62437=CARTESIAN_POINT('Ctrl Pts',(-1.9302496520377,-2.01120346334021,15.2152115919387));
#62438=CARTESIAN_POINT('Ctrl Pts',(-1.94128816753001,-2.0011886687103,15.2146701535858));
#62439=CARTESIAN_POINT('Ctrl Pts',(-1.95224352654855,-1.99108137253609,
15.2141289446068));
#62440=CARTESIAN_POINT('Ctrl Pts',(-1.96311133771197,-1.98088698275119,
15.2135881466736));
#62441=CARTESIAN_POINT('Ctrl Pts',(-2.03178675603926,-1.91646702066845,
15.2101707589647));
#62442=CARTESIAN_POINT('Ctrl Pts',(-2.09701995613675,-1.8485265277173,15.2067672577273));
#62443=CARTESIAN_POINT('Ctrl Pts',(-2.15871310631003,-1.77747212767664,
15.2033732357386));
#62444=CARTESIAN_POINT('Ctrl Pts',(-2.22164945390415,-1.7049858888237,15.1999108197811));
#62445=CARTESIAN_POINT('Ctrl Pts',(-2.28090217022322,-1.62925832538052,
15.19645826896));
#62446=CARTESIAN_POINT('Ctrl Pts',(-2.33633512040192,-1.55067589533689,
15.1930109042136));
#62447=CARTESIAN_POINT('Ctrl Pts',(-2.39218601791983,-1.47150097801918,
15.1895375474008));
#62448=CARTESIAN_POINT('Ctrl Pts',(-2.44415984798534,-1.38942718616138,
15.1860694551604));
#62449=CARTESIAN_POINT('Ctrl Pts',(-2.49207710040016,-1.30481547317471,
15.1826018417945));
#62450=CARTESIAN_POINT('Ctrl Pts',(-2.52022211747796,-1.25511733759765,
15.1805650798249));
#62451=CARTESIAN_POINT('Ctrl Pts',(-2.54696681998739,-1.20454303320315,
15.1785284830672));
#62452=CARTESIAN_POINT('Ctrl Pts',(-2.57226731600719,-1.15316195438398,
15.1764910817393));
#62453=CARTESIAN_POINT('Ctrl Pts',(-2.57933924906923,-1.13880004030214,
15.1759215922795));
#62454=CARTESIAN_POINT('Ctrl Pts',(-2.58629893239321,-1.12437358425022,
15.1753519825172));
#62455=CARTESIAN_POINT('Ctrl Pts',(-2.59313735551554,-1.10990147500019,
15.1747829112963));
#62456=CARTESIAN_POINT('Ctrl Pts',(-2.63517066423893,-1.02094666405867,
15.1712850367298));
#62457=CARTESIAN_POINT('Ctrl Pts',(-2.6726976453638,-0.930127060905838,
15.167801819036));
#62458=CARTESIAN_POINT('Ctrl Pts',(-2.70558302354023,-0.837840896222647,
15.1643285389057));
#62459=CARTESIAN_POINT('Ctrl Pts',(-2.73847376195491,-0.745539689114618,
15.1608546926391));
#62460=CARTESIAN_POINT('Ctrl Pts',(-2.76672184052432,-0.651770570287676,
15.1573907871758));
#62461=CARTESIAN_POINT('Ctrl Pts',(-2.79014819101862,-0.556903769359717,
15.1539321008988));
#62462=CARTESIAN_POINT('Ctrl Pts',(-2.81305355218475,-0.464146754627161,
15.1505503339286));
#62463=CARTESIAN_POINT('Ctrl Pts',(-2.83134952927604,-0.370339481518358,
15.1471735565822));
#62464=CARTESIAN_POINT('Ctrl Pts',(-2.8448219024633,-0.275813943398833,
15.1437973553073));
#62465=CARTESIAN_POINT('Ctrl Pts',(-2.85447686455589,-0.208072315799913,
15.1413778042102));
#62466=CARTESIAN_POINT('Ctrl Pts',(-2.86165354894421,-0.139961477196466,
15.1389585489751));
#62467=CARTESIAN_POINT('Ctrl Pts',(-2.86625656775569,-0.071602632167948,
15.1365379651471));
#62468=CARTESIAN_POINT('Ctrl Pts',(-2.8678889837078,-0.0473598311579388,
15.1356795285827));
#62469=CARTESIAN_POINT('Ctrl Pts',(-2.86919553394546,-0.0231160969724086,
15.1348219958471));
#62470=CARTESIAN_POINT('Ctrl Pts',(-2.87017396612668,0.00112290304428943,
15.1339652973708));
#62471=CARTESIAN_POINT('',(0.261080338132197,2.92584241055005,15.058));
#62472=CARTESIAN_POINT('Ctrl Pts',(0.260984867623723,2.92515103163649,15.058));
#62473=CARTESIAN_POINT('Ctrl Pts',(0.163110290089364,2.92129299518303,15.0703787026841));
#62474=CARTESIAN_POINT('Ctrl Pts',(0.0656985383021158,2.91278590387498,
15.0828015605825));
#62475=CARTESIAN_POINT('Ctrl Pts',(-0.0308724856851826,2.89964343902045,
15.0952881213498));
#62476=CARTESIAN_POINT('Ctrl Pts',(-0.13093434020212,2.88602590291106,15.1082260438789));
#62477=CARTESIAN_POINT('Ctrl Pts',(-0.230094798512676,2.86743186329655,
15.121232357953));
#62478=CARTESIAN_POINT('Ctrl Pts',(-0.327908726704405,2.84382209488468,
15.1343288085909));
#62479=CARTESIAN_POINT('Ctrl Pts',(-0.401269172848201,2.82611476857578,
15.1441511465694));
#62480=CARTESIAN_POINT('Ctrl Pts',(-0.473871776581697,2.80558493098147,
15.154024186365));
#62481=CARTESIAN_POINT('Ctrl Pts',(-0.54551386023679,2.78219703023119,15.1639571016578));
#62482=CARTESIAN_POINT('Ctrl Pts',(-0.599245422978111,2.76465610466849,
15.1714067881273));
#62483=CARTESIAN_POINT('Ctrl Pts',(-0.652436445713434,2.74550717996222,
15.178890154564));
#62484=CARTESIAN_POINT('Ctrl Pts',(-0.704995275147146,2.7247296345796,15.186411071114));
#62485=CARTESIAN_POINT('Ctrl Pts',(-0.720729468886594,2.71850959642421,
15.1886625588158));
#62486=CARTESIAN_POINT('Ctrl Pts',(-0.736406966678059,2.71214357207348,
15.1909174117022));
#62487=CARTESIAN_POINT('Ctrl Pts',(-0.752025204049111,2.70563092815761,
15.1931757336031));
#62488=CARTESIAN_POINT('Ctrl Pts',(-0.764775912501757,2.70031401422844,
15.1950194246335));
#62489=CARTESIAN_POINT('Ctrl Pts',(-0.777478081511626,2.69490314594757,
15.196864120682));
#62490=CARTESIAN_POINT('Ctrl Pts',(-0.790130440968904,2.6893983882733,15.1987098648068));
#62491=CARTESIAN_POINT('Ctrl Pts',(-0.873485337988913,2.65313254310755,
15.2108697952897));
#62492=CARTESIAN_POINT('Ctrl Pts',(-0.954683148186728,2.61279395749136,
15.2230755503321));
#62493=CARTESIAN_POINT('Ctrl Pts',(-1.0333900295422,2.56835839969231,15.2353460721376));
#62494=CARTESIAN_POINT('Ctrl Pts',(-1.07474974365993,2.54500793864519,15.2417941141031));
#62495=CARTESIAN_POINT('Ctrl Pts',(-1.11542111238663,2.52052546068703,15.2482600407761));
#62496=CARTESIAN_POINT('Ctrl Pts',(-1.15535178122673,2.49490314259947,15.2547466008415));
#62497=CARTESIAN_POINT('Ctrl Pts',(-1.23327915249916,2.44489947493076,15.2674055567063));
#62498=CARTESIAN_POINT('Ctrl Pts',(-1.30838829429154,2.39055588937394,15.2801430971848));
#62499=CARTESIAN_POINT('Ctrl Pts',(-1.38046450469962,2.33219918561456,15.2929796526032));
#62500=CARTESIAN_POINT('Ctrl Pts',(-1.45426350057602,2.27244762382022,15.3061230309111));
#62501=CARTESIAN_POINT('Ctrl Pts',(-1.52488347180723,2.20848778279982,15.3193702140928));
#62502=CARTESIAN_POINT('Ctrl Pts',(-1.59204074405781,2.14065188994946,15.332743132764));
#62503=CARTESIAN_POINT('Ctrl Pts',(-1.60237109058904,2.13021715582588,15.3348001979094));
#62504=CARTESIAN_POINT('Ctrl Pts',(-1.61262065491134,2.1196893711682,15.3368604944486));
#62505=CARTESIAN_POINT('Ctrl Pts',(-1.62278430900332,2.10907388768773,15.3389232952054));
#62506=CARTESIAN_POINT('Ctrl Pts',(-1.68486768809848,2.04423056665054,15.3515236493914));
#62507=CARTESIAN_POINT('Ctrl Pts',(-1.74353795945352,1.97633977637267,15.3641743680265));
#62508=CARTESIAN_POINT('Ctrl Pts',(-1.79863355499942,1.90572574364455,15.3768970731667));
#62509=CARTESIAN_POINT('Ctrl Pts',(-1.8536060338742,1.83526950510231,15.3895913481376));
#62510=CARTESIAN_POINT('Ctrl Pts',(-1.90502010402237,1.76210117952091,15.4023572882508));
#62511=CARTESIAN_POINT('Ctrl Pts',(-1.95266740197694,1.68652354076833,15.4152163709358));
#62512=CARTESIAN_POINT('Ctrl Pts',(-1.999553014057,1.61215408007279,15.4278698893587));
#62513=CARTESIAN_POINT('Ctrl Pts',(-2.04279147033365,1.53545080587127,15.4406135962167));
#62514=CARTESIAN_POINT('Ctrl Pts',(-2.08213462636226,1.45669772176484,15.4534679553077));
#62515=CARTESIAN_POINT('Ctrl Pts',(-2.10370638024081,1.41351760306046,15.4605159681915));
#62516=CARTESIAN_POINT('Ctrl Pts',(-2.12410620181193,1.36972125073741,15.4675972464718));
#62517=CARTESIAN_POINT('Ctrl Pts',(-2.14328646703913,1.32535636167276,15.4747151632939));
#62518=CARTESIAN_POINT('Ctrl Pts',(-2.15012579550102,1.30953666132481,15.4772532810172));
#62519=CARTESIAN_POINT('Ctrl Pts',(-2.15681001155505,1.29364468163272,15.4797960573454));
#62520=CARTESIAN_POINT('Ctrl Pts',(-2.16333680365848,1.27768262506038,15.4823436452153));
#62521=CARTESIAN_POINT('Ctrl Pts',(-2.16791412260327,1.2664882400105,15.4841302996752));
#62522=CARTESIAN_POINT('Ctrl Pts',(-2.17241292255598,1.25526195256421,15.4859189101699));
#62523=CARTESIAN_POINT('Ctrl Pts',(-2.17682958710993,1.24401228867859,15.4877083034276));
#62524=CARTESIAN_POINT('Ctrl Pts',(-2.20791015801245,1.16484712416239,15.5003004673422));
#62525=CARTESIAN_POINT('Ctrl Pts',(-2.2349734122897,1.08441291813616,15.5129492481641));
#62526=CARTESIAN_POINT('Ctrl Pts',(-2.25783961089921,1.00297802743715,15.5256767231474));
#62527=CARTESIAN_POINT('Ctrl Pts',(-2.28035828534265,0.922780797311416,
15.5382107639178));
#62528=CARTESIAN_POINT('Ctrl Pts',(-2.29880657051476,0.841612257746407,
15.5508211250137));
#62529=CARTESIAN_POINT('Ctrl Pts',(-2.31296316132111,0.759731453145844,
15.5635288923091));
#62530=CARTESIAN_POINT('Ctrl Pts',(-2.32670958827523,0.680223009708963,
15.5758684730222));
#62531=CARTESIAN_POINT('Ctrl Pts',(-2.33640931253598,0.600042348520933,
15.5882998973352));
#62532=CARTESIAN_POINT('Ctrl Pts',(-2.34181299591968,0.519439649300842,
15.6008424709262));
#62533=CARTESIAN_POINT('Ctrl Pts',(-2.34572284670801,0.461119332452094,
15.609917686434));
#62534=CARTESIAN_POINT('Ctrl Pts',(-2.34738263953658,0.402578305857885,
15.6190510917899));
#62535=CARTESIAN_POINT('Ctrl Pts',(-2.34668236863854,0.343918483395394,
15.62825));
#62536=CARTESIAN_POINT('',(-2.14373220034752,2.0119373894844,15.058));
#62537=CARTESIAN_POINT('Origin',(0.,0.,15.058));
#62538=CARTESIAN_POINT('Ctrl Pts',(-2.87017396612668,0.00112290304428943,
15.1339652973708));
#62539=CARTESIAN_POINT('Ctrl Pts',(-2.87266912500978,0.0629362380616879,
15.1317805789463));
#62540=CARTESIAN_POINT('Ctrl Pts',(-2.87303098230106,0.124718621761705,
15.1296012856735));
#62541=CARTESIAN_POINT('Ctrl Pts',(-2.87121685856479,0.18637804904607,15.1274262638706));
#62542=CARTESIAN_POINT('Ctrl Pts',(-2.86841400163638,0.281643079490827,
15.1240658123162));
#62543=CARTESIAN_POINT('Ctrl Pts',(-2.86041988710444,0.376614623554742,
15.1207155571276));
#62544=CARTESIAN_POINT('Ctrl Pts',(-2.84750858059062,0.47099184224787,15.1173712434175));
#62545=CARTESIAN_POINT('Ctrl Pts',(-2.83433033308302,0.567320307975548,
15.1139577860911));
#62546=CARTESIAN_POINT('Ctrl Pts',(-2.81602924148459,0.663030385704492,
15.1105505184628));
#62547=CARTESIAN_POINT('Ctrl Pts',(-2.79284156103339,0.757800921120369,
15.1071449162423));
#62548=CARTESIAN_POINT('Ctrl Pts',(-2.77879319434313,0.815218101582043,
15.1050816159094));
#62549=CARTESIAN_POINT('Ctrl Pts',(-2.76295010551778,0.872290339259573,
15.1030189268812));
#62550=CARTESIAN_POINT('Ctrl Pts',(-2.74535586092349,0.928944130664371,
15.100955843023));
#62551=CARTESIAN_POINT('Ctrl Pts',(-2.7354097693855,0.960970728468381,15.099789574088));
#62552=CARTESIAN_POINT('Ctrl Pts',(-2.72490394590206,0.992863566804536,
15.098623178978));
#62553=CARTESIAN_POINT('Ctrl Pts',(-2.7138453785436,1.0246089965303,15.0974564759315));
#62554=CARTESIAN_POINT('Ctrl Pts',(-2.70868377697821,1.03942621963478,15.0969119156755));
#62555=CARTESIAN_POINT('Ctrl Pts',(-2.7034040983514,1.05420445638712,15.0963675402945));
#62556=CARTESIAN_POINT('Ctrl Pts',(-2.69801003661965,1.06893536837389,15.0958235919881));
#62557=CARTESIAN_POINT('Ctrl Pts',(-2.66394262772994,1.16197175299988,15.0923881642358));
#62558=CARTESIAN_POINT('Ctrl Pts',(-2.62528653689294,1.25320878716493,15.0889665364856));
#62559=CARTESIAN_POINT('Ctrl Pts',(-2.58232115247044,1.34232723597939,15.0855542358814));
#62560=CARTESIAN_POINT('Ctrl Pts',(-2.53887733631532,1.43243804397901,15.0821039383428));
#62561=CARTESIAN_POINT('Ctrl Pts',(-2.49102735184572,1.52038366982231,15.0786631768276));
#62562=CARTESIAN_POINT('Ctrl Pts',(-2.43900735397324,1.60582293428401,15.0752273273902));
#62563=CARTESIAN_POINT('Ctrl Pts',(-2.38725398360023,1.69082428143753,15.071809088333));
#62564=CARTESIAN_POINT('Ctrl Pts',(-2.33137274895099,1.77334571203064,15.0683957111292));
#62565=CARTESIAN_POINT('Ctrl Pts',(-2.27155099682431,1.8530278346518,15.064982642569));
#62566=CARTESIAN_POINT('Ctrl Pts',(-2.23076137590659,1.90735930205439,15.0626554326866));
#62567=CARTESIAN_POINT('Ctrl Pts',(-2.18813878650124,1.96037022431859,15.0603283662998));
#62568=CARTESIAN_POINT('Ctrl Pts',(-2.14373220034752,2.0119373894844,15.058));
#62569=CARTESIAN_POINT('',(-2.,-2.44929359829471E-16,16.));
#62570=CARTESIAN_POINT('',(-2.5,-3.06161699786838E-16,15.5));
#62571=CARTESIAN_POINT('Origin',(0.,0.,16.));
#62572=CARTESIAN_POINT('Ctrl Pts',(1.70810875200393,-2.39535560853239,-0.329233991005387));
#62573=CARTESIAN_POINT('Ctrl Pts',(2.5000696979919,-1.83061464970825,-0.276613620635017));
#62574=CARTESIAN_POINT('Ctrl Pts',(3.46698259537958,0.135843711197753,-0.171372879894276));
#62575=CARTESIAN_POINT('Ctrl Pts',(1.78000461065578,2.98198357260362,-0.013511768783165));
#62576=CARTESIAN_POINT('Ctrl Pts',(-1.52068059202578,3.11864337292237,0.144349342327946));
#62577=CARTESIAN_POINT('Ctrl Pts',(-3.44323740053193,0.434868872546417,
0.302210453439058));
#62578=CARTESIAN_POINT('Ctrl Pts',(-2.24748662857037,-2.64500439253867,
0.460071564550167));
#62579=CARTESIAN_POINT('Ctrl Pts',(0.98413688813967,-3.32800743087112,0.61793267566128));
#62580=CARTESIAN_POINT('Ctrl Pts',(3.3242675736315,-0.997273536182889,0.775793786772391));
#62581=CARTESIAN_POINT('Ctrl Pts',(2.65350107828341,2.23705783115145,0.933654897883501));
#62582=CARTESIAN_POINT('Ctrl Pts',(-0.420704297245377,3.44500822120461,
1.09151600899461));
#62583=CARTESIAN_POINT('Ctrl Pts',(-3.11384086799285,1.53272940938773,1.24937712010572));
#62584=CARTESIAN_POINT('Ctrl Pts',(-2.98662452021757,-1.76786447124123,
1.40723823121684));
#62585=CARTESIAN_POINT('Ctrl Pts',(-0.154268773033873,-3.46719137695888,
1.56509934232795));
#62586=CARTESIAN_POINT('Ctrl Pts',(2.81781362814421,-2.02612228753563,1.72296045343906));
#62587=CARTESIAN_POINT('Ctrl Pts',(3.23766264061691,1.25011350527631,1.88082156455017));
#62588=CARTESIAN_POINT('Ctrl Pts',(0.724998218776244,3.39405562633926,2.03868267566128));
#62589=CARTESIAN_POINT('Ctrl Pts',(-2.44433298400306,2.46383378430329,2.19654378677239));
#62590=CARTESIAN_POINT('Ctrl Pts',(-3.39970985401105,-0.698006346200326,
2.35440489788351));
#62591=CARTESIAN_POINT('Ctrl Pts',(-1.27579956793912,-3.22762676650925,
2.51226600899461));
#62592=CARTESIAN_POINT('Ctrl Pts',(2.00366607964198,-2.83382462640088,2.67012712010573));
#62593=CARTESIAN_POINT('Ctrl Pts',(3.46831127903076,0.12671419166248,2.82798823121683));
#62594=CARTESIAN_POINT('Ctrl Pts',(1.79153366111842,2.9724815653929,2.98584934232795));
#62595=CARTESIAN_POINT('Ctrl Pts',(-1.50792549309295,3.12592391504671,3.14371045343906));
#62596=CARTESIAN_POINT('Ctrl Pts',(-3.44158119482194,0.448060782465637,
3.30157156455017));
#62597=CARTESIAN_POINT('Ctrl Pts',(-2.25802486298351,-2.63563337612261,
3.45943267566128));
#62598=CARTESIAN_POINT('Ctrl Pts',(0.970737398643871,-3.33210271331857,
3.61729378677239));
#62599=CARTESIAN_POINT('Ctrl Pts',(3.32025430017048,-1.01052014634333,3.7751548978835));
#62600=CARTESIAN_POINT('Ctrl Pts',(2.66245099976358,2.22634100195603,3.93301600899462));
#62601=CARTESIAN_POINT('Ctrl Pts',(-0.406867188726441,3.44669387613558,
4.09087712010572));
#62602=CARTESIAN_POINT('Ctrl Pts',(-3.10766543711734,1.54520390729755,4.24873823121684));
#62603=CARTESIAN_POINT('Ctrl Pts',(-2.99369583814259,-1.75585443953709,
4.40659934232795));
#62604=CARTESIAN_POINT('Ctrl Pts',(-0.16818635164463,-3.46654769699322,
4.56446045343906));
#62605=CARTESIAN_POINT('Ctrl Pts',(2.80965791624474,-2.03741551431062,4.72232156455017));
#62606=CARTESIAN_POINT('Ctrl Pts',(3.24265463709948,1.23710569022097,4.88018267566128));
#62607=CARTESIAN_POINT('Ctrl Pts',(0.738617048059715,3.39111846455234,5.0380437867724));
#62608=CARTESIAN_POINT('Ctrl Pts',(-2.43442290318405,2.47362582310745,5.1959048978835));
#62609=CARTESIAN_POINT('Ctrl Pts',(-3.40248440570545,-0.684353310232048,
5.35376600899462));
#62610=CARTESIAN_POINT('Ctrl Pts',(-1.28874579170717,-3.22247945977245,
5.51162712010572));
#62611=CARTESIAN_POINT('Ctrl Pts',(1.99227427239527,-2.84184496548404,5.66948823121683));
#62612=CARTESIAN_POINT('Ctrl Pts',(3.46879199270663,0.112790494414327,5.82734934232795));
#62613=CARTESIAN_POINT('Ctrl Pts',(1.803451502182,2.96526596843754,5.98521045343906));
#62614=CARTESIAN_POINT('Ctrl Pts',(-1.49536511544646,3.13195190828366,6.14307156455017));
#62615=CARTESIAN_POINT('Ctrl Pts',(-3.4397548386282,0.461872530499354,6.30093267566129));
#62616=CARTESIAN_POINT('Ctrl Pts',(-2.26858675213732,-2.62654787360198,
6.45879378677239));
#62617=CARTESIAN_POINT('Ctrl Pts',(0.957353695793138,-3.33597264458916,
6.61665489788351));
#62618=CARTESIAN_POINT('Ctrl Pts',(3.31617107144768,-1.02384032406894,6.77451600899461));
#62619=CARTESIAN_POINT('Ctrl Pts',(2.67136662968815,2.21563532967061,6.93237712010573));
#62620=CARTESIAN_POINT('Ctrl Pts',(-0.393028031746144,3.44829937078522,
7.09023823121684));
#62621=CARTESIAN_POINT('Ctrl Pts',(-3.10143756889894,1.55766639256237,7.24809934232795));
#62622=CARTESIAN_POINT('Ctrl Pts',(-3.00072015011765,-1.74382285940228,
7.40596045343905));
#62623=CARTESIAN_POINT('Ctrl Pts',(-0.182100573498421,-3.46584462511342,
7.56382156455018));
#62624=CARTESIAN_POINT('Ctrl Pts',(2.80145659039814,-2.04867775807003,7.72168267566128));
#62625=CARTESIAN_POINT('Ctrl Pts',(3.24759455782818,1.22407890769377,7.8795437867724));
#62626=CARTESIAN_POINT('Ctrl Pts',(0.752223882355328,3.38812615100299,8.03740489788349));
#62627=CARTESIAN_POINT('Ctrl Pts',(-2.42447354494764,2.4833782664236,8.19526600899462));
#62628=CARTESIAN_POINT('Ctrl Pts',(-3.40520415435994,-0.670689385204343,
8.35312712010572));
#62629=CARTESIAN_POINT('Ctrl Pts',(-1.30167123501543,-3.21728015258687,
8.51098823121684));
#62630=CARTESIAN_POINT('Ctrl Pts',(1.98085035420065,-2.84981954842042,8.66884934232795));
#62631=CARTESIAN_POINT('Ctrl Pts',(3.46921681308078,0.098864999537257,8.82671045343906));
#62632=CARTESIAN_POINT('Ctrl Pts',(1.81534028008778,2.95800257805621,8.98457156455017));
#62633=CARTESIAN_POINT('Ctrl Pts',(-1.4827806401293,3.13792943795007,9.14243267566127));
#62634=CARTESIAN_POINT('Ctrl Pts',(-3.4378730539225,0.475676832953572,9.3002937867724));
#62635=CARTESIAN_POINT('Ctrl Pts',(-2.27911208446667,-2.61742004476474,
9.45815489788349));
#62636=CARTESIAN_POINT('Ctrl Pts',(0.943954565772613,-3.3397888199782,9.61601600899462));
#62637=CARTESIAN_POINT('Ctrl Pts',(3.31203440522278,-1.03714400297725,9.77387712010572));
#62638=CARTESIAN_POINT('Ctrl Pts',(2.68023921253269,2.20489395389312,9.93173823121684));
#62639=CARTESIAN_POINT('Ctrl Pts',(-0.379182541400898,3.44984929882113,
10.0895993423279));
#62640=CARTESIAN_POINT('Ctrl Pts',(-3.09515972337558,1.57010377716378,10.2474604534391));
#62641=CARTESIAN_POINT('Ctrl Pts',(-3.00769610777576,-1.73176317886687,
10.4053215645502));
#62642=CARTESIAN_POINT('Ctrl Pts',(-0.196011860918037,-3.46508570377902,
10.5631826756613));
#62643=CARTESIAN_POINT('Ctrl Pts',(2.79321012116224,-2.05990698897259,10.7210437867724));
#62644=CARTESIAN_POINT('Ctrl Pts',(3.25248214612884,1.2110324001305,10.8789048978835));
#62645=CARTESIAN_POINT('Ctrl Pts',(0.765818594962506,3.38507924024569,11.0367660089946));
#62646=CARTESIAN_POINT('Ctrl Pts',(-2.41448511783304,2.49309069223908,11.1946271201057));
#62647=CARTESIAN_POINT('Ctrl Pts',(-3.40786903136843,-0.657014653010787,
11.3524882312168));
#62648=CARTESIAN_POINT('Ctrl Pts',(-1.3145757016765,-3.21202900045202,11.510349342328));
#62649=CARTESIAN_POINT('Ctrl Pts',(1.96939451380669,-2.85774821044889,11.668210453439));
#62650=CARTESIAN_POINT('Ctrl Pts',(3.46958573405997,0.0849379149034097,
11.8260715645502));
#62651=CARTESIAN_POINT('Ctrl Pts',(1.82719979676502,2.95069151525923,11.9839326756613));
#62652=CARTESIAN_POINT('Ctrl Pts',(-1.47017225488226,3.14385641459579,12.1417937867724));
#62653=CARTESIAN_POINT('Ctrl Pts',(-3.43593590116163,0.489473446687968,
12.2996548978835));
#62654=CARTESIAN_POINT('Ctrl Pts',(-2.28960063207268,-2.60824999320481,
12.4575160089946));
#62655=CARTESIAN_POINT('Ctrl Pts',(0.930540112760845,-3.34355126315401,
12.6153771201057));
#62656=CARTESIAN_POINT('Ctrl Pts',(3.30784458181684,-1.05043080491032,12.7732382312169));
#62657=CARTESIAN_POINT('Ctrl Pts',(2.68906819704165,2.19411673426304,12.9310993423279));
#62658=CARTESIAN_POINT('Ctrl Pts',(-0.365330160772045,3.45134423437463,
13.0889604534391));
#62659=CARTESIAN_POINT('Ctrl Pts',(-3.08883349189378,1.58251471600082,13.2468215645502));
#62660=CARTESIAN_POINT('Ctrl Pts',(-3.01462075186278,-1.71967340539697,
13.4046826756613));
#62661=CARTESIAN_POINT('Ctrl Pts',(-0.209925428309919,-3.46427512302224,
13.5625437867724));
#62662=CARTESIAN_POINT('Ctrl Pts',(2.78492903121011,-2.07109504482717,13.7204048978835));
#62663=CARTESIAN_POINT('Ctrl Pts',(3.25729747472216,1.19795113049603,13.8782660089946));
#62664=CARTESIAN_POINT('Ctrl Pts',(0.779438885227093,3.38200690959721,14.0361271201057));
#62665=CARTESIAN_POINT('Ctrl Pts',(-2.40453022224261,2.50270729758603,14.1939882312168));
#62666=CARTESIAN_POINT('Ctrl Pts',(-3.41034060095634,-0.643223025084935,
14.351849342328));
#62667=CARTESIAN_POINT('Ctrl Pts',(-1.3277234162215,-3.20692920286191,14.5097104534391));
#62668=CARTESIAN_POINT('Ctrl Pts',(1.95841253548915,-2.86524258546647,14.6675715645502));
#62669=CARTESIAN_POINT('Ctrl Pts',(3.46892903525912,0.0702659147297645,
14.8254326756613));
#62670=CARTESIAN_POINT('Ctrl Pts',(1.8409162673649,2.94476989555806,14.9832937867724));
#62671=CARTESIAN_POINT('Ctrl Pts',(-1.46144261101867,3.14684084841223,15.1411548978835));
#62672=CARTESIAN_POINT('Ctrl Pts',(-2.76985851330384,1.3890220685151,15.2463956386242));
#62673=CARTESIAN_POINT('Ctrl Pts',(-2.91090525077878,0.426608275808748,
15.2990160089946));
#62674=CARTESIAN_POINT('Ctrl Pts',(1.59774743137963,-2.24059110187414,-0.219489327336926));
#62675=CARTESIAN_POINT('Ctrl Pts',(2.33853958862414,-1.71233819332979,-0.166868956966556));
#62676=CARTESIAN_POINT('Ctrl Pts',(3.24298000926863,0.127066816079881,-0.061628216225815));
#62677=CARTESIAN_POINT('Ctrl Pts',(1.66499808117169,2.78931689094975,0.0962328948852963));
#62678=CARTESIAN_POINT('Ctrl Pts',(-1.42242905026252,2.9171470684346,0.254094005996407));
#62679=CARTESIAN_POINT('Ctrl Pts',(-3.22076899721748,0.406771889250497,
0.411955117107519));
#62680=CARTESIAN_POINT('Ctrl Pts',(-2.10227597256058,-2.4741100174146,0.56981622821863));
#62681=CARTESIAN_POINT('Ctrl Pts',(0.9205515651778,-3.11298406383574,0.72767733932974));
#62682=CARTESIAN_POINT('Ctrl Pts',(3.10948583967916,-0.932839451205724,
0.885538450440853));
#62683=CARTESIAN_POINT('Ctrl Pts',(2.48205773023319,2.09252098227156,1.04339956155196));
#62684=CARTESIAN_POINT('Ctrl Pts',(-0.393522490594119,3.22242540473713,
1.20126067266308));
#62685=CARTESIAN_POINT('Ctrl Pts',(-2.91265485451303,1.43369939061326,1.35912178377418));
#62686=CARTESIAN_POINT('Ctrl Pts',(-2.79365798581306,-1.65364231910831,
1.5169828948853));
#62687=CARTESIAN_POINT('Ctrl Pts',(-0.144301430203291,-3.24317530141947,
1.67484400599641));
#62688=CARTESIAN_POINT('Ctrl Pts',(2.6357540064074,-1.8952140352733,1.83270511710752));
#62689=CARTESIAN_POINT('Ctrl Pts',(3.02847647238534,1.16934336859111,1.99056622821863));
#62690=CARTESIAN_POINT('Ctrl Pts',(0.67815590807408,3.17476486938028,2.14842733932974));
#62691=CARTESIAN_POINT('Ctrl Pts',(-2.28640403724036,2.30464488610489,2.30628845044085));
#62692=CARTESIAN_POINT('Ctrl Pts',(-3.18005377603123,-0.652907986929923,
2.46414956155196));
#62693=CARTESIAN_POINT('Ctrl Pts',(-1.19336984851725,-3.01908901853714,
2.62201067266307));
#62694=CARTESIAN_POINT('Ctrl Pts',(1.87420872841654,-2.65073053018457,2.77987178377419));
#62695=CARTESIAN_POINT('Ctrl Pts',(3.24422284634695,0.118527157015377,2.9377328948853));
#62696=CARTESIAN_POINT('Ctrl Pts',(1.67578223688854,2.78042881072881,3.09559400599641));
#62697=CARTESIAN_POINT('Ctrl Pts',(-1.41049806136441,2.92395721296701,3.25345511710752));
#62698=CARTESIAN_POINT('Ctrl Pts',(-3.21921979935999,0.419111466671254,
3.41131622821863));
#62699=CARTESIAN_POINT('Ctrl Pts',(-2.11213332909314,-2.46534446464132,
3.56917733932974));
#62700=CARTESIAN_POINT('Ctrl Pts',(0.908017819947236,-3.11681474909129,
3.72703845044085));
#62701=CARTESIAN_POINT('Ctrl Pts',(3.10573186478955,-0.94523019467185,3.88489956155197));
#62702=CARTESIAN_POINT('Ctrl Pts',(2.49042939511648,2.08249657000891,4.04276067266307));
#62703=CARTESIAN_POINT('Ctrl Pts',(-0.380579401011611,3.2240021490943,4.20062178377419));
#62704=CARTESIAN_POINT('Ctrl Pts',(-2.90687841972373,1.44536790818848,4.3584828948853));
#62705=CARTESIAN_POINT('Ctrl Pts',(-2.8002724241724,-1.64240825846459,4.5163440059964));
#62706=CARTESIAN_POINT('Ctrl Pts',(-0.157319790685473,-3.24257320977247,
4.67420511710753));
#62707=CARTESIAN_POINT('Ctrl Pts',(2.62812523703122,-1.90577760392813,4.83206622821863));
#62708=CARTESIAN_POINT('Ctrl Pts',(3.03314593476479,1.15717599162043,4.98992733932975));
#62709=CARTESIAN_POINT('Ctrl Pts',(0.690894821495446,3.17201747832858,5.14778845044085));
#62710=CARTESIAN_POINT('Ctrl Pts',(-2.27713424914591,2.31380425890769,5.30564956155197));
#62711=CARTESIAN_POINT('Ctrl Pts',(-3.18264906326793,-0.640137076925948,
5.46351067266308));
#62712=CARTESIAN_POINT('Ctrl Pts',(-1.20547961362863,-3.01427428053665,
5.62137178377419));
#62713=CARTESIAN_POINT('Ctrl Pts',(1.86355294859817,-2.65823267321491,5.7792328948853));
#62714=CARTESIAN_POINT('Ctrl Pts',(3.24467250099567,0.105503073222438,5.93709400599641));
#62715=CARTESIAN_POINT('Ctrl Pts',(1.68693006335134,2.77367941524228,6.09495511710752));
#62716=CARTESIAN_POINT('Ctrl Pts',(-1.39874921276312,2.92959573609933,6.25281622821863));
#62717=CARTESIAN_POINT('Ctrl Pts',(-3.21751144448276,0.432030834315646,
6.41067733932974));
#62718=CARTESIAN_POINT('Ctrl Pts',(-2.12201281202782,-2.45684597864148,
6.56853845044085));
#62719=CARTESIAN_POINT('Ctrl Pts',(0.895498841382776,-3.12043464316416,
6.72639956155197));
#62720=CARTESIAN_POINT('Ctrl Pts',(3.10191245446456,-0.957689752484927,
6.88426067266308));
#62721=CARTESIAN_POINT('Ctrl Pts',(2.4987689840299,2.07248259380561,7.04212178377418));
#62722=CARTESIAN_POINT('Ctrl Pts',(-0.367634395319329,3.22550391234535,
7.1999828948853));
#62723=CARTESIAN_POINT('Ctrl Pts',(-2.90105293558095,1.45702518925863,7.3578440059964));
#62724=CARTESIAN_POINT('Ctrl Pts',(-2.8068428936476,-1.63115404163953,7.51570511710752));
#62725=CARTESIAN_POINT('Ctrl Pts',(-0.170335011291572,-3.24191556353729,
7.67356622821863));
#62726=CARTESIAN_POINT('Ctrl Pts',(2.62045380083611,-1.91631219138755,7.83142733932975));
#62727=CARTESIAN_POINT('Ctrl Pts',(3.03776668601744,1.14499087267086,7.98928845044085));
#62728=CARTESIAN_POINT('Ctrl Pts',(0.703622514928034,3.16921849888318,8.14714956155197));
#62729=CARTESIAN_POINT('Ctrl Pts',(-2.26782772135753,2.32292659449655,8.30501067266308));
#62730=CARTESIAN_POINT('Ctrl Pts',(-3.18519308830241,-0.627355981407313,
8.46287178377418));
#62731=CARTESIAN_POINT('Ctrl Pts',(-1.21756994091078,-3.00941090184898,
8.62073289488531));
#62732=CARTESIAN_POINT('Ctrl Pts',(1.852867132528,-2.6656920164142,8.77859400599641));
#62733=CARTESIAN_POINT('Ctrl Pts',(3.24506987362244,0.0924773079458306,
8.93645511710752));
#62734=CARTESIAN_POINT('Ctrl Pts',(1.698050704434,2.7668853142746,9.09431622821864));
#62735=CARTESIAN_POINT('Ctrl Pts',(-1.3869778234475,2.93518705612466,9.25217733932973));
#62736=CARTESIAN_POINT('Ctrl Pts',(-3.21575124234316,0.444943237441223,
9.41003845044086));
#62737=CARTESIAN_POINT('Ctrl Pts',(-2.13185810008334,-2.44830790103859,
9.56789956155196));
#62738=CARTESIAN_POINT('Ctrl Pts',(0.882965432401702,-3.12400425453603,
9.72576067266308));
#62739=CARTESIAN_POINT('Ctrl Pts',(3.09804305924746,-0.970133877473286,
9.88362178377418));
#62740=CARTESIAN_POINT('Ctrl Pts',(2.50706830714555,2.06243522092151,10.0414828948853));
#62741=CARTESIAN_POINT('Ctrl Pts',(-0.354683465462343,3.22695369915506,
10.1993440059964));
#62742=CARTESIAN_POINT('Ctrl Pts',(-2.89518070317902,1.4686589914253,10.3572051171075));
#62743=CARTESIAN_POINT('Ctrl Pts',(-2.81336813298999,-1.61987353998757,
10.5150662282186));
#62744=CARTESIAN_POINT('Ctrl Pts',(-0.183347487058001,-3.24120567629433,
10.6729273393297));
#62745=CARTESIAN_POINT('Ctrl Pts',(2.61274013797703,-1.9268158989588,10.8307884504409));
#62746=CARTESIAN_POINT('Ctrl Pts',(3.04233848605292,1.13278730312457,10.988649561552));
#62747=CARTESIAN_POINT('Ctrl Pts',(0.716338869857416,3.16636844976869,11.1465106726631));
#62748=CARTESIAN_POINT('Ctrl Pts',(-2.25848464894066,2.33201149812516,11.3043717837742));
#62749=CARTESIAN_POINT('Ctrl Pts',(-3.18768578696123,-0.61456477697643,
11.4622328948853));
#62750=CARTESIAN_POINT('Ctrl Pts',(-1.22964064685199,-3.00449902792679,
11.6200940059964));
#62751=CARTESIAN_POINT('Ctrl Pts',(1.84215145675955,-2.67310840566659,11.7779551171075));
#62752=CARTESIAN_POINT('Ctrl Pts',(3.24541495852771,0.0794500556270124,
11.9358162282186));
#62753=CARTESIAN_POINT('Ctrl Pts',(1.70914397486321,2.76004662101762,12.0936773393297));
#62754=CARTESIAN_POINT('Ctrl Pts',(-1.37518406902836,2.94073108937221,12.2515384504409));
#62755=CARTESIAN_POINT('Ctrl Pts',(-3.21393924949186,0.457848448617044,
12.409399561552));
#62756=CARTESIAN_POINT('Ctrl Pts',(-2.14166898008542,-2.43973032873338,
12.5672606726631));
#62757=CARTESIAN_POINT('Ctrl Pts',(0.870417690451563,-3.12752360534598,
12.7251217837742));
#62758=CARTESIAN_POINT('Ctrl Pts',(3.09412394134766,-0.98256221591188,12.8829828948853));
#62759=CARTESIAN_POINT('Ctrl Pts',(2.51532684882466,2.05235432006483,13.0408440059964));
#62760=CARTESIAN_POINT('Ctrl Pts',(-0.341726090504644,3.22835204655998,
13.1987051171075));
#62761=CARTESIAN_POINT('Ctrl Pts',(-2.88926321104715,1.48026805649486,13.3565662282186));
#62762=CARTESIAN_POINT('Ctrl Pts',(-2.81984537414356,-1.60856488971291,
13.5144273393297));
#62763=CARTESIAN_POINT('Ctrl Pts',(-0.196362095487134,-3.24044746735677,
13.6722884504409));
#62764=CARTESIAN_POINT('Ctrl Pts',(2.60499409125458,-1.93728109181189,13.830149561552));
#62765=CARTESIAN_POINT('Ctrl Pts',(3.04684269509828,1.12055121749295,13.9880106726631));
#62766=CARTESIAN_POINT('Ctrl Pts',(0.729079149865556,3.16349462314833,14.1458717837742));
#62767=CARTESIAN_POINT('Ctrl Pts',(-2.24917294156805,2.34100677226896,14.3037328948853));
#62768=CARTESIAN_POINT('Ctrl Pts',(-3.1899976678388,-0.601664229474863,
14.4615940059964));
#62769=CARTESIAN_POINT('Ctrl Pts',(-1.24193888437236,-2.9997287294955,14.6194551171075));
#62770=CARTESIAN_POINT('Ctrl Pts',(1.83187902672385,-2.68011856729716,14.7773162282186));
#62771=CARTESIAN_POINT('Ctrl Pts',(3.24480068919561,0.0657260169420378,
14.9351773393297));
#62772=CARTESIAN_POINT('Ctrl Pts',(1.72197422097186,2.75450759860113,15.0930384504409));
#62773=CARTESIAN_POINT('Ctrl Pts',(-1.36701844957144,2.94352269819615,15.250899561552));
#62774=CARTESIAN_POINT('Ctrl Pts',(-2.59089728316432,1.29927701587847,15.3561403022927));
#62775=CARTESIAN_POINT('Ctrl Pts',(-2.72283095673204,0.399045011670964,
15.4087606726631));
#62776=CARTESIAN_POINT('Ctrl Pts',(1.48738611075532,-2.0858265952159,-0.109744663668465));
#62777=CARTESIAN_POINT('Ctrl Pts',(2.17700947925639,-1.59406173695134,-0.0571242932980945));
#62778=CARTESIAN_POINT('Ctrl Pts',(3.01897742315769,0.118289920962009,0.0481164474426461));
#62779=CARTESIAN_POINT('Ctrl Pts',(1.5499915516876,2.59665020929587,0.205977558553758));
#62780=CARTESIAN_POINT('Ctrl Pts',(-1.32417750849926,2.71565076394683,0.363838669664868));
#62781=CARTESIAN_POINT('Ctrl Pts',(-2.99830059390304,0.37867490595458,0.521699780775981));
#62782=CARTESIAN_POINT('Ctrl Pts',(-1.95706531655079,-2.30321564229053,
0.679560891887089));
#62783=CARTESIAN_POINT('Ctrl Pts',(0.856966242215927,-2.89796069680035,
0.837422002998203));
#62784=CARTESIAN_POINT('Ctrl Pts',(2.89470410572683,-0.86840536622856,0.995283114109312));
#62785=CARTESIAN_POINT('Ctrl Pts',(2.31061438218297,1.94798413339166,1.15314422522042));
#62786=CARTESIAN_POINT('Ctrl Pts',(-0.36634068394286,2.99984258826965,1.31100533633153));
#62787=CARTESIAN_POINT('Ctrl Pts',(-2.71146884103322,1.33466937183879,1.46886644744265));
#62788=CARTESIAN_POINT('Ctrl Pts',(-2.60069145140856,-1.53942016697539,
1.62672755855376));
#62789=CARTESIAN_POINT('Ctrl Pts',(-0.134334087372704,-3.01915922588007,
1.78458866966487));
#62790=CARTESIAN_POINT('Ctrl Pts',(2.45369438467058,-1.76430578301097,1.94244978077598));
#62791=CARTESIAN_POINT('Ctrl Pts',(2.81929030415377,1.0885732319059,2.10031089188709));
#62792=CARTESIAN_POINT('Ctrl Pts',(0.63131359737191,2.95547411242131,2.2581720029982));
#62793=CARTESIAN_POINT('Ctrl Pts',(-2.12847509047765,2.14545598790649,2.41603311410931));
#62794=CARTESIAN_POINT('Ctrl Pts',(-2.96039769805142,-0.607809627659522,
2.57389422522043));
#62795=CARTESIAN_POINT('Ctrl Pts',(-1.11094012909538,-2.81055127056503,
2.73175533633153));
#62796=CARTESIAN_POINT('Ctrl Pts',(1.74475137719111,-2.46763643396825,2.88961644744264));
#62797=CARTESIAN_POINT('Ctrl Pts',(3.02013441366314,0.110340122368272,3.04747755855376));
#62798=CARTESIAN_POINT('Ctrl Pts',(1.56003081265866,2.58837605606472,3.20533866966487));
#62799=CARTESIAN_POINT('Ctrl Pts',(-1.31307062963587,2.72199051088731,3.36319978077598));
#62800=CARTESIAN_POINT('Ctrl Pts',(-2.99685840389804,0.390162150876873,
3.52106089188709));
#62801=CARTESIAN_POINT('Ctrl Pts',(-1.96624179520275,-2.29505555316004,
3.6789220029982));
#62802=CARTESIAN_POINT('Ctrl Pts',(0.845298241250599,-2.90152678486402,
3.83678311410932));
#62803=CARTESIAN_POINT('Ctrl Pts',(2.89120942940861,-0.879940243000373,
3.99464422522043));
#62804=CARTESIAN_POINT('Ctrl Pts',(2.31840779046938,1.93865213806179,4.15250533633154));
#62805=CARTESIAN_POINT('Ctrl Pts',(-0.354291613296782,3.00131042205302,
4.31036644744265));
#62806=CARTESIAN_POINT('Ctrl Pts',(-2.70609140233011,1.34553190907942,4.46822755855376));
#62807=CARTESIAN_POINT('Ctrl Pts',(-2.60684901020221,-1.52896207739209,
4.62608866966487));
#62808=CARTESIAN_POINT('Ctrl Pts',(-0.146453229726317,-3.01859872255171,
4.78394978077598));
#62809=CARTESIAN_POINT('Ctrl Pts',(2.44659255781772,-1.77413969354566,4.94181089188709));
#62810=CARTESIAN_POINT('Ctrl Pts',(2.82363723243009,1.07724629301989,5.09967200299821));
#62811=CARTESIAN_POINT('Ctrl Pts',(0.643172594931182,2.95291649210482,5.25753311410931));
#62812=CARTESIAN_POINT('Ctrl Pts',(-2.11984559510778,2.15398269470792,5.41539422522043));
#62813=CARTESIAN_POINT('Ctrl Pts',(-2.96281372083041,-0.595920843619846,
5.57325533633153));
#62814=CARTESIAN_POINT('Ctrl Pts',(-1.12221343555009,-2.80606910130085,
5.73111644744265));
#62815=CARTESIAN_POINT('Ctrl Pts',(1.73483162480106,-2.47462038094578,5.88897755855376));
#62816=CARTESIAN_POINT('Ctrl Pts',(3.02055300928471,0.0982156520305535,
6.04683866966487));
#62817=CARTESIAN_POINT('Ctrl Pts',(1.57040862452068,2.58209286204701,6.20469978077598));
#62818=CARTESIAN_POINT('Ctrl Pts',(-1.30213331007977,2.72723956391501,6.36256089188709));
#62819=CARTESIAN_POINT('Ctrl Pts',(-2.99526805033731,0.402189138131933,
6.52042200299821));
#62820=CARTESIAN_POINT('Ctrl Pts',(-1.97543887191833,-2.28714408368097,
6.67828311410931));
#62821=CARTESIAN_POINT('Ctrl Pts',(0.833643986972413,-2.90489664173917,
6.83614422522043));
#62822=CARTESIAN_POINT('Ctrl Pts',(2.88765383748144,-0.891539180900916,
6.99400533633154));
#62823=CARTESIAN_POINT('Ctrl Pts',(2.32617133837164,1.9293298579406,7.15186644744265));
#62824=CARTESIAN_POINT('Ctrl Pts',(-0.342240758892514,3.00270845390548,
7.30972755855377));
#62825=CARTESIAN_POINT('Ctrl Pts',(-2.70066830226297,1.35638398595488,7.46758866966487));
#62826=CARTESIAN_POINT('Ctrl Pts',(-2.61296563717754,-1.51848522387679,
7.62544978077598));
#62827=CARTESIAN_POINT('Ctrl Pts',(-0.158569449084724,-3.01798650196116,
7.78331089188708));
#62828=CARTESIAN_POINT('Ctrl Pts',(2.43945101127409,-1.78394662470507,7.94117200299821));
#62829=CARTESIAN_POINT('Ctrl Pts',(2.8279388142067,1.06590283764795,8.09903311410931));
#62830=CARTESIAN_POINT('Ctrl Pts',(0.655021147500741,2.95031084676337,8.25689422522044));
#62831=CARTESIAN_POINT('Ctrl Pts',(-2.11118189776743,2.16247492256949,8.41475533633153));
#62832=CARTESIAN_POINT('Ctrl Pts',(-2.96518202224487,-0.584022577610279,
8.57261644744266));
#62833=CARTESIAN_POINT('Ctrl Pts',(-1.13346864680612,-2.8015416511111,8.73047755855375));
#62834=CARTESIAN_POINT('Ctrl Pts',(1.72488391085535,-2.48156448440799,8.88833866966489));
#62835=CARTESIAN_POINT('Ctrl Pts',(3.0209229341641,0.0860896163543999,9.04619978077597));
#62836=CARTESIAN_POINT('Ctrl Pts',(1.58076112878023,2.575768050493,9.2040608918871));
#62837=CARTESIAN_POINT('Ctrl Pts',(-1.2911750067657,2.73244467429924,9.3619220029982));
#62838=CARTESIAN_POINT('Ctrl Pts',(-2.99362943076381,0.414209641928883,
9.51978311410932));
#62839=CARTESIAN_POINT('Ctrl Pts',(-1.98460411570002,-2.27919575731244,
9.67764422522042));
#62840=CARTESIAN_POINT('Ctrl Pts',(0.821976299030791,-2.90821968909385,
9.83550533633154));
#62841=CARTESIAN_POINT('Ctrl Pts',(2.88405171327213,-0.903123751969326,
9.99336644744264));
#62842=CARTESIAN_POINT('Ctrl Pts',(2.33389740175841,1.9199764879499,10.1512275585538));
#62843=CARTESIAN_POINT('Ctrl Pts',(-0.330184389523787,3.00405809948898,
10.3090886696649));
#62844=CARTESIAN_POINT('Ctrl Pts',(-2.69520168298246,1.36721420568682,10.466949780776));
#62845=CARTESIAN_POINT('Ctrl Pts',(-2.61904015820422,-1.50798390110827,
10.6248108918871));
#62846=CARTESIAN_POINT('Ctrl Pts',(-0.170683113197963,-3.01732564880962,
10.7826720029982));
#62847=CARTESIAN_POINT('Ctrl Pts',(2.43227015479182,-1.793724808945,10.9405331141093));
#62848=CARTESIAN_POINT('Ctrl Pts',(2.83219482597701,1.05454220611865,11.0983942252204));
#62849=CARTESIAN_POINT('Ctrl Pts',(0.666859144752323,2.94765765929168,11.2562553363315));
#62850=CARTESIAN_POINT('Ctrl Pts',(-2.10248418004828,2.17093230401124,11.4141164474427));
#62851=CARTESIAN_POINT('Ctrl Pts',(-2.96750254255404,-0.572114900942073,
11.5719775585538));
#62852=CARTESIAN_POINT('Ctrl Pts',(-1.14470559202747,-2.79696905540156,
11.7298386696649));
#62853=CARTESIAN_POINT('Ctrl Pts',(1.7149083997124,-2.48846860088429,11.887699780776));
#62854=CARTESIAN_POINT('Ctrl Pts',(3.02124418299545,0.0739621963506113,
12.0455608918871));
#62855=CARTESIAN_POINT('Ctrl Pts',(1.5910881529614,2.56940172677601,12.2034220029982));
#62856=CARTESIAN_POINT('Ctrl Pts',(-1.28019588317448,2.73760576414863,12.3612831141093));
#62857=CARTESIAN_POINT('Ctrl Pts',(-2.99194259782208,0.42622345054612,12.5191442252204));
#62858=CARTESIAN_POINT('Ctrl Pts',(-1.99373732809816,-2.27121066426194,
12.6770053363315));
#62859=CARTESIAN_POINT('Ctrl Pts',(0.810295268142284,-2.91149594753796,
12.8348664474426));
#62860=CARTESIAN_POINT('Ctrl Pts',(2.88040330087848,-0.914693626913434,
12.9927275585538));
#62861=CARTESIAN_POINT('Ctrl Pts',(2.34158550060768,1.91059190586663,13.1505886696649));
#62862=CARTESIAN_POINT('Ctrl Pts',(-0.318122020237242,3.00535985874532,
13.308449780776));
#62863=CARTESIAN_POINT('Ctrl Pts',(-2.68969293020052,1.37802139698889,13.4663108918871));
#62864=CARTESIAN_POINT('Ctrl Pts',(-2.62506999642434,-1.49745637402886,
13.6241720029982));
#62865=CARTESIAN_POINT('Ctrl Pts',(-0.182798762664348,-3.0166198116913,
13.7820331141093));
#62866=CARTESIAN_POINT('Ctrl Pts',(2.42505915129906,-1.80346713879661,13.9398942252204));
#62867=CARTESIAN_POINT('Ctrl Pts',(2.8363879154744,1.04315130448987,14.0977553363316));
#62868=CARTESIAN_POINT('Ctrl Pts',(0.678719414504022,2.94498233669946,14.2556164474426));
#62869=CARTESIAN_POINT('Ctrl Pts',(-2.09381566089348,2.17930624695187,14.4134775585538));
#62870=CARTESIAN_POINT('Ctrl Pts',(-2.96965473472126,-0.560105433864789,
14.5713386696649));
#62871=CARTESIAN_POINT('Ctrl Pts',(-1.15615435252323,-2.79252825612909,
14.729199780776));
#62872=CARTESIAN_POINT('Ctrl Pts',(1.70534551795855,-2.49499454912784,14.8870608918871));
#62873=CARTESIAN_POINT('Ctrl Pts',(3.0206723431321,0.0611861191543108,15.0449220029982));
#62874=CARTESIAN_POINT('Ctrl Pts',(1.60303217457882,2.56424530164419,15.2027831141093));
#62875=CARTESIAN_POINT('Ctrl Pts',(-1.27259428812422,2.74020454798006,15.3606442252204));
#62876=CARTESIAN_POINT('Ctrl Pts',(-2.41193605302479,1.20953196324185,15.4658849659612));
#62877=CARTESIAN_POINT('Ctrl Pts',(-2.53475666268529,0.371481747533179,
15.5185053363315));
#62878=CARTESIAN_POINT('Ctrl Pts',(1.37702479013102,-1.93106208855765,-3.60822483003176E-15));
#62879=CARTESIAN_POINT('Ctrl Pts',(2.01547936988864,-1.47578528057288,0.0526203703703667));
#62880=CARTESIAN_POINT('Ctrl Pts',(2.79497483704674,0.109513025844136,0.157861111111108));
#62881=CARTESIAN_POINT('Ctrl Pts',(1.4349850222035,2.40398352764199,0.315722222222219));
#62882=CARTESIAN_POINT('Ctrl Pts',(-1.225925966736,2.51415445945906,0.473583333333329));
#62883=CARTESIAN_POINT('Ctrl Pts',(-2.77583219058859,0.350577922658662,
0.631444444444441));
#62884=CARTESIAN_POINT('Ctrl Pts',(-1.811854660541,-2.13232126716645,0.789305555555552));
#62885=CARTESIAN_POINT('Ctrl Pts',(0.793380919254056,-2.68293732976497,
0.947166666666663));
#62886=CARTESIAN_POINT('Ctrl Pts',(2.67992237177449,-0.803971281251394,
1.10502777777777));
#62887=CARTESIAN_POINT('Ctrl Pts',(2.13917103413275,1.80344728451176,1.26288888888888));
#62888=CARTESIAN_POINT('Ctrl Pts',(-0.339158877291603,2.77725977180218,
1.42075));
#62889=CARTESIAN_POINT('Ctrl Pts',(-2.51028282755341,1.23563935306431,1.57861111111111));
#62890=CARTESIAN_POINT('Ctrl Pts',(-2.40772491700405,-1.42519801484247,
1.73647222222222));
#62891=CARTESIAN_POINT('Ctrl Pts',(-0.124366744542119,-2.79514315034066,
1.89433333333333));
#62892=CARTESIAN_POINT('Ctrl Pts',(2.27163476293377,-1.63339753074864,2.05219444444444));
#62893=CARTESIAN_POINT('Ctrl Pts',(2.61010413592219,1.00780309522069,2.21005555555555));
#62894=CARTESIAN_POINT('Ctrl Pts',(0.584471286669745,2.73618335546233,2.36791666666667));
#62895=CARTESIAN_POINT('Ctrl Pts',(-1.97054614371495,1.98626708970809,2.52577777777777));
#62896=CARTESIAN_POINT('Ctrl Pts',(-2.7407416200716,-0.562711268389121,
2.68363888888889));
#62897=CARTESIAN_POINT('Ctrl Pts',(-1.02851040967351,-2.60201352259292,
2.84149999999999));
#62898=CARTESIAN_POINT('Ctrl Pts',(1.61529402596567,-2.28454233775194,2.99936111111111));
#62899=CARTESIAN_POINT('Ctrl Pts',(2.79604598097933,0.102153087721166,3.15722222222222));
#62900=CARTESIAN_POINT('Ctrl Pts',(1.44427938842878,2.39632330140064,3.31508333333333));
#62901=CARTESIAN_POINT('Ctrl Pts',(-1.21564319790733,2.5200238088076,3.47294444444445));
#62902=CARTESIAN_POINT('Ctrl Pts',(-2.77449700843608,0.361212835082494,
3.63080555555555));
#62903=CARTESIAN_POINT('Ctrl Pts',(-1.82035026131238,-2.12476664167876,
3.78866666666667));
#62904=CARTESIAN_POINT('Ctrl Pts',(0.782578662553965,-2.68623882063674,
3.94652777777777));
#62905=CARTESIAN_POINT('Ctrl Pts',(2.67668699402767,-0.814650291328897,
4.10438888888889));
#62906=CARTESIAN_POINT('Ctrl Pts',(2.14638618582228,1.79480770611467,4.26225));
#62907=CARTESIAN_POINT('Ctrl Pts',(-0.328003825581952,2.77861869501174,
4.42011111111111));
#62908=CARTESIAN_POINT('Ctrl Pts',(-2.50530438493649,1.24569590997036,4.57797222222222));
#62909=CARTESIAN_POINT('Ctrl Pts',(-2.41342559623202,-1.41551589631959,
4.73583333333333));
#62910=CARTESIAN_POINT('Ctrl Pts',(-0.135586668767159,-2.79462423533096,
4.89369444444444));
#62911=CARTESIAN_POINT('Ctrl Pts',(2.2650598786042,-1.64250178316317,5.05155555555556));
#62912=CARTESIAN_POINT('Ctrl Pts',(2.61412853009539,0.997316594419356,5.20941666666666));
#62913=CARTESIAN_POINT('Ctrl Pts',(0.595450368366912,2.73381550588105,5.36727777777778));
#62914=CARTESIAN_POINT('Ctrl Pts',(-1.96255694106964,1.99416113050815,5.52513888888888));
#62915=CARTESIAN_POINT('Ctrl Pts',(-2.74297837839289,-0.551704610313744,
5.683));
#62916=CARTESIAN_POINT('Ctrl Pts',(-1.03894725747156,-2.59786392206505,
5.84086111111111));
#62917=CARTESIAN_POINT('Ctrl Pts',(1.60611030100396,-2.29100808867664,5.99872222222222));
#62918=CARTESIAN_POINT('Ctrl Pts',(2.79643351757374,0.090928230838667,6.15658333333333));
#62919=CARTESIAN_POINT('Ctrl Pts',(1.45388718569001,2.39050630885174,6.31444444444444));
#62920=CARTESIAN_POINT('Ctrl Pts',(-1.20551740739643,2.52488339173069,6.47230555555556));
#62921=CARTESIAN_POINT('Ctrl Pts',(-2.77302465619186,0.372347441948222,
6.63016666666666));
#62922=CARTESIAN_POINT('Ctrl Pts',(-1.82886493180883,-2.11744218872047,
6.78802777777778));
#62923=CARTESIAN_POINT('Ctrl Pts',(0.771789132562049,-2.68935864031417,
6.94588888888888));
#62924=CARTESIAN_POINT('Ctrl Pts',(2.67339522049833,-0.825388609316905,
7.10375));
#62925=CARTESIAN_POINT('Ctrl Pts',(2.15357369271338,1.7861771220756,7.26161111111111));
#62926=CARTESIAN_POINT('Ctrl Pts',(-0.3168471224657,2.77991299546561,7.41947222222222));
#62927=CARTESIAN_POINT('Ctrl Pts',(-2.50028366894498,1.25574278265114,7.57733333333334));
#62928=CARTESIAN_POINT('Ctrl Pts',(-2.41908838070749,-1.40581640611404,
7.73519444444443));
#62929=CARTESIAN_POINT('Ctrl Pts',(-0.146803886877873,-2.79405744038503,
7.89305555555557));
#62930=CARTESIAN_POINT('Ctrl Pts',(2.25844822171206,-1.65158105802259,8.05091666666665));
#62931=CARTESIAN_POINT('Ctrl Pts',(2.61811094239596,0.986814802625037,8.20877777777778));
#62932=CARTESIAN_POINT('Ctrl Pts',(0.606419780073446,2.73140319464357,8.36663888888888));
#62933=CARTESIAN_POINT('Ctrl Pts',(-1.95453607417732,2.00202325064244,8.52450000000001));
#62934=CARTESIAN_POINT('Ctrl Pts',(-2.74517095618734,-0.540689173813247,
8.68236111111111));
#62935=CARTESIAN_POINT('Ctrl Pts',(-1.04936735270146,-2.59367240037321,
8.84022222222223));
#62936=CARTESIAN_POINT('Ctrl Pts',(1.59690068918271,-2.29743695240177,8.99808333333332));
#62937=CARTESIAN_POINT('Ctrl Pts',(2.79677599470576,0.0797019247629725,
9.15594444444445));
#62938=CARTESIAN_POINT('Ctrl Pts',(1.46347155312646,2.38465078671139,9.31380555555555));
#62939=CARTESIAN_POINT('Ctrl Pts',(-1.19537219008389,2.52970229247383,9.47166666666666));
#62940=CARTESIAN_POINT('Ctrl Pts',(-2.77150761918447,0.383476046416537,
9.62952777777778));
#62941=CARTESIAN_POINT('Ctrl Pts',(-1.83735013131669,-2.1100836135863,9.78738888888888));
#62942=CARTESIAN_POINT('Ctrl Pts',(0.760987165659879,-2.69243512365168,
9.94525));
#62943=CARTESIAN_POINT('Ctrl Pts',(2.6700603672968,-0.836113626465368,10.1031111111111));
#62944=CARTESIAN_POINT('Ctrl Pts',(2.16072649637127,1.7775177549783,10.2609722222222));
#62945=CARTESIAN_POINT('Ctrl Pts',(-0.305685313585232,2.78116249982291,
10.4188333333333));
#62946=CARTESIAN_POINT('Ctrl Pts',(-2.4952226627859,1.26576941994835,10.5766944444444));
#62947=CARTESIAN_POINT('Ctrl Pts',(-2.42471218341845,-1.39609426222898,
10.7345555555556));
#62948=CARTESIAN_POINT('Ctrl Pts',(-0.158018739337926,-2.79344562132492,
10.8924166666667));
#62949=CARTESIAN_POINT('Ctrl Pts',(2.25180017160661,-1.66063371893121,11.0502777777778));
#62950=CARTESIAN_POINT('Ctrl Pts',(2.62205116590109,0.976297109112734,11.2081388888889));
#62951=CARTESIAN_POINT('Ctrl Pts',(0.617379419647229,2.72894686881467,11.366));
#62952=CARTESIAN_POINT('Ctrl Pts',(-1.9464837111559,2.00985310989732,11.5238611111111));
#62953=CARTESIAN_POINT('Ctrl Pts',(-2.74731929814685,-0.529665024907718,
11.6817222222222));
#62954=CARTESIAN_POINT('Ctrl Pts',(-1.05977053720295,-2.58943908287633,
11.8395833333333));
#62955=CARTESIAN_POINT('Ctrl Pts',(1.58766534266525,-2.30382879610199,11.9974444444444));
#62956=CARTESIAN_POINT('Ctrl Pts',(2.79707340746319,0.0684743370742143,
12.1553055555555));
#62957=CARTESIAN_POINT('Ctrl Pts',(1.47303233105958,2.37875683253439,12.3131666666667));
#62958=CARTESIAN_POINT('Ctrl Pts',(-1.18520769732058,2.53448043892505,12.4710277777778));
#62959=CARTESIAN_POINT('Ctrl Pts',(-2.76994594615232,0.394598452475193,
12.6288888888889));
#62960=CARTESIAN_POINT('Ctrl Pts',(-1.8458056761109,-2.1026909997905,12.78675));
#62961=CARTESIAN_POINT('Ctrl Pts',(0.750172845833004,-2.69546828972993,
12.9446111111111));
#62962=CARTESIAN_POINT('Ctrl Pts',(2.66668266040929,-0.846825037914988,
13.1024722222222));
#62963=CARTESIAN_POINT('Ctrl Pts',(2.16784415239069,1.76882949166842,13.2603333333333));
#62964=CARTESIAN_POINT('Ctrl Pts',(-0.294517949969841,2.78236767093066,
13.4181944444444));
#62965=CARTESIAN_POINT('Ctrl Pts',(-2.49012264935389,1.27577473748293,13.5760555555556));
#62966=CARTESIAN_POINT('Ctrl Pts',(-2.43029461870512,-1.3863478583448,13.7339166666666));
#62967=CARTESIAN_POINT('Ctrl Pts',(-0.16923542984156,-2.79279215602584,
13.8917777777778));
#62968=CARTESIAN_POINT('Ctrl Pts',(2.24512421134353,-1.66965318578134,14.0496388888889));
#62969=CARTESIAN_POINT('Ctrl Pts',(2.62593313585052,0.965751391486786,14.2075));
#62970=CARTESIAN_POINT('Ctrl Pts',(0.628359679142483,2.72647005025058,14.3653611111111));
#62971=CARTESIAN_POINT('Ctrl Pts',(-1.93845838021891,2.01760572163479,14.5232222222222));
#62972=CARTESIAN_POINT('Ctrl Pts',(-2.74931180160372,-0.518546638254714,
14.6810833333333));
#62973=CARTESIAN_POINT('Ctrl Pts',(-1.07036982067409,-2.58532778276268,
14.8389444444444));
#62974=CARTESIAN_POINT('Ctrl Pts',(1.57881200919325,-2.30987053095853,14.9968055555556));
#62975=CARTESIAN_POINT('Ctrl Pts',(2.79654399706859,0.0566462213665858,
15.1546666666667));
#62976=CARTESIAN_POINT('Ctrl Pts',(1.48409012818578,2.37398300468726,15.3125277777778));
#62977=CARTESIAN_POINT('Ctrl Pts',(-1.17817012667699,2.53688639776398,15.4703888888889));
#62978=CARTESIAN_POINT('Ctrl Pts',(-2.23297482288527,1.11978691060522,15.5756296296296));
#62979=CARTESIAN_POINT('Ctrl Pts',(-2.34668236863854,0.343918483395395,
15.62825));
#62980=CARTESIAN_POINT('',(1.37702479013102,-1.93106208855765,0.));
#62981=CARTESIAN_POINT('Ctrl Pts',(1.37702479013102,-1.93106208855765,-3.60822483003176E-15));
#62982=CARTESIAN_POINT('Ctrl Pts',(2.01547936988864,-1.47578528057288,0.0526203703703667));
#62983=CARTESIAN_POINT('Ctrl Pts',(2.79497483704674,0.109513025844136,0.157861111111108));
#62984=CARTESIAN_POINT('Ctrl Pts',(1.4349850222035,2.40398352764199,0.315722222222219));
#62985=CARTESIAN_POINT('Ctrl Pts',(-1.225925966736,2.51415445945906,0.473583333333329));
#62986=CARTESIAN_POINT('Ctrl Pts',(-2.32453883371355,0.980556500150706,
0.585479295290919));
#62987=CARTESIAN_POINT('Ctrl Pts',(-2.37485146083742,0.100616720091163,
0.644754886878137));
#62988=CARTESIAN_POINT('Ctrl Pts',(-2.37409249406917,0.00172857025301858,
0.651410108094986));
#62989=CARTESIAN_POINT('Ctrl Pts',(1.29200104020317,2.64812001020929,8.84708972748172E-17));
#62990=CARTESIAN_POINT('Ctrl Pts',(1.36315737313149,2.60529414881161,1.11522009070411E-16));
#62991=CARTESIAN_POINT('Ctrl Pts',(1.43224767624703,2.55934891308958,-5.0435019692162E-16));
#62992=CARTESIAN_POINT('Ctrl Pts',(1.49903325513988,2.51027466650741,-4.38885039422132E-16));
#62993=CARTESIAN_POINT('Ctrl Pts',(1.57786836962904,2.45234638450537,-3.65724347932505E-16));
#62994=CARTESIAN_POINT('Ctrl Pts',(1.65349331585608,2.39005818913334,-5.19266877679362E-16));
#62995=CARTESIAN_POINT('Ctrl Pts',(1.72573019513852,2.32378926839401,-6.48786580015326E-16));
#62996=CARTESIAN_POINT('Ctrl Pts',(1.76374109312884,2.28891869797108,-7.16939582223243E-16));
#62997=CARTESIAN_POINT('Ctrl Pts',(1.80081318017132,2.2529453987339,-5.63901193634668E-16));
#62998=CARTESIAN_POINT('Ctrl Pts',(1.83691551656788,2.21592189026143,-5.759281940243E-16));
#62999=CARTESIAN_POINT('Ctrl Pts',(1.85077163488616,2.20171222503873,-5.80544170635404E-16));
#63000=CARTESIAN_POINT('Ctrl Pts',(1.86448486767998,2.18734784556943,1.18680337545582E-16));
#63001=CARTESIAN_POINT('Ctrl Pts',(1.87805332095389,2.17283167229843,1.45716771982052E-16));
#63002=CARTESIAN_POINT('Ctrl Pts',(1.88973877018296,2.16033002584437,1.69001141656681E-16));
#63003=CARTESIAN_POINT('Ctrl Pts',(1.90131548250979,2.14771713833219,-1.20552840767492E-16));
#63004=CARTESIAN_POINT('Ctrl Pts',(1.91277473204616,2.1350036118777,-1.04083408558608E-16));
#63005=CARTESIAN_POINT('Ctrl Pts',(1.9778462733255,2.06280963801715,-1.05614606835039E-17));
#63006=CARTESIAN_POINT('Ctrl Pts',(2.03920496551099,1.98729716595704,-4.81412066085989E-16));
#63007=CARTESIAN_POINT('Ctrl Pts',(2.09668120715734,1.90884345828848,-3.33066907387547E-16));
#63008=CARTESIAN_POINT('Ctrl Pts',(2.14417843271961,1.84401087107344,-2.10477411937863E-16));
#63009=CARTESIAN_POINT('Ctrl Pts',(2.18902362087598,1.7771688452355,-1.7119245770294E-16));
#63010=CARTESIAN_POINT('Ctrl Pts',(2.23109606376114,1.7085204430367,-1.94289029309402E-16));
#63011=CARTESIAN_POINT('Ctrl Pts',(2.24950275752339,1.67848676707472,-2.0439377938723E-16));
#63012=CARTESIAN_POINT('Ctrl Pts',(2.26737842523222,1.6481072631063,-4.61788465798711E-16));
#63013=CARTESIAN_POINT('Ctrl Pts',(2.28471149018554,1.61739870311764,-5.13478148889135E-16));
#63014=CARTESIAN_POINT('Ctrl Pts',(2.29518347047447,1.59884575614786,-5.44707094486553E-16));
#63015=CARTESIAN_POINT('Ctrl Pts',(2.30545737670969,1.58017269818218,-5.13081578012294E-16));
#63016=CARTESIAN_POINT('Ctrl Pts',(2.3155304906665,1.56138322284078,-5.55111512312578E-16));
#63017=CARTESIAN_POINT('Ctrl Pts',(2.32274660107223,1.54792294341672,-5.85220637212436E-16));
#63018=CARTESIAN_POINT('Ctrl Pts',(2.32985933504635,1.5344033850802,-2.08590721469464E-17));
#63019=CARTESIAN_POINT('Ctrl Pts',(2.33686168047272,1.52083799385098,-2.77555756156289E-17));
#63020=CARTESIAN_POINT('Ctrl Pts',(2.38047027627073,1.43635663411551,-7.07050181056999E-17));
#63021=CARTESIAN_POINT('Ctrl Pts',(2.41986655819018,1.34997905359849,1.3198210981114E-16));
#63022=CARTESIAN_POINT('Ctrl Pts',(2.45488985599288,1.26205357875123,5.55111512312578E-17));
#63023=CARTESIAN_POINT('Ctrl Pts',(2.48959846523414,1.17491812491653,-2.02727065483809E-17));
#63024=CARTESIAN_POINT('Ctrl Pts',(2.52001253380174,1.08626153918075,-4.44579204063227E-16));
#63025=CARTESIAN_POINT('Ctrl Pts',(2.54592562425351,0.996413712953991,-4.9960036108132E-16));
#63026=CARTESIAN_POINT('Ctrl Pts',(2.57101139534936,0.909434430942866,-5.528648743571E-16));
#63027=CARTESIAN_POINT('Ctrl Pts',(2.59187898968551,0.821337996875181,-7.89241560757653E-18));
#63028=CARTESIAN_POINT('Ctrl Pts',(2.60829286172102,0.732427405689614,-8.32667268468867E-17));
#63029=CARTESIAN_POINT('Ctrl Pts',(2.61783087340729,0.680761945161682,-1.27066328786625E-16));
#63030=CARTESIAN_POINT('Ctrl Pts',(2.62586408863254,0.628821695636964,-4.14952786105416E-17));
#63031=CARTESIAN_POINT('Ctrl Pts',(2.63233843305125,0.576668196894126,-5.55111512312578E-17));
#63032=CARTESIAN_POINT('Ctrl Pts',(2.63414224296016,0.562137768524485,-5.94160979378542E-17));
#63033=CARTESIAN_POINT('Ctrl Pts',(2.63582527555606,0.547588319420663,3.76279563716787E-16));
#63034=CARTESIAN_POINT('Ctrl Pts',(2.63738542604938,0.533029261526728,3.60822483003176E-16));
#63035=CARTESIAN_POINT('Ctrl Pts',(2.64690685377435,0.444176924476997,2.66489610960485E-16));
#63036=CARTESIAN_POINT('Ctrl Pts',(2.65183263786108,0.355196731300303,5.62349138697447E-16));
#63037=CARTESIAN_POINT('Ctrl Pts',(2.65198717743404,0.266381980286723,3.88578058618805E-16));
#63038=CARTESIAN_POINT('Ctrl Pts',(2.65207998114243,0.213047173573617,2.84225494854879E-16));
#63039=CARTESIAN_POINT('Ctrl Pts',(2.65045121279133,0.159772024909719,-3.854419951949E-17));
#63040=CARTESIAN_POINT('Ctrl Pts',(2.64705383408491,0.106621318043217,-8.32667268468867E-17));
#63041=CARTESIAN_POINT('Ctrl Pts',(2.64128166054733,0.0163178428672467,
-1.29468843946197E-16));
#63042=CARTESIAN_POINT('Ctrl Pts',(2.63040647827402,-0.0736278476965388,
-4.84995897836269E-16));
#63043=CARTESIAN_POINT('Ctrl Pts',(2.61462343406994,-0.162881882998066,
-6.10622663543836E-16));
#63044=CARTESIAN_POINT('Ctrl Pts',(2.59852152905154,-0.253939094797703,
-7.38787434739808E-16));
#63045=CARTESIAN_POINT('Ctrl Pts',(2.57731092756958,-0.344277415185344,
-3.0810955291451E-16));
#63046=CARTESIAN_POINT('Ctrl Pts',(2.55115372858487,-0.433510589178544,
-3.60822483003176E-16));
#63047=CARTESIAN_POINT('Ctrl Pts',(2.54730992415644,-0.446623417870874,
-3.68568656216471E-16));
#63048=CARTESIAN_POINT('Ctrl Pts',(2.54335838534963,-0.4597150170452,-1.33461876853334E-16));
#63049=CARTESIAN_POINT('Ctrl Pts',(2.53930241226215,-0.472774949708627,
-1.38777878078145E-16));
#63050=CARTESIAN_POINT('Ctrl Pts',(2.51300579541719,-0.557448106523011,
-1.73243798916645E-16));
#63051=CARTESIAN_POINT('Ctrl Pts',(2.48237490705721,-0.640633082262047,
2.2266366763076E-16));
#63052=CARTESIAN_POINT('Ctrl Pts',(2.4476284488952,-0.722031078376524,1.66533453693773E-16));
#63053=CARTESIAN_POINT('Ctrl Pts',(2.41285997251409,-0.803480654968775,
1.10367671027941E-16));
#63054=CARTESIAN_POINT('Ctrl Pts',(2.37397005509887,-0.883141781461701,
-2.60473824643759E-16));
#63055=CARTESIAN_POINT('Ctrl Pts',(2.33113438836321,-0.960686402199183,
-2.22044604925031E-16));
#63056=CARTESIAN_POINT('Ctrl Pts',(2.28891526223189,-1.03711491080453,-1.84168503113759E-16));
#63057=CARTESIAN_POINT('Ctrl Pts',(2.24286247138705,-1.11148803969701,-4.86311355035046E-16));
#63058=CARTESIAN_POINT('Ctrl Pts',(2.19311210725222,-1.18345333925267,-6.10622663543836E-16));
#63059=CARTESIAN_POINT('Ctrl Pts',(2.16658994742807,-1.22181838863071,-6.76893623556989E-16));
#63060=CARTESIAN_POINT('Ctrl Pts',(2.13901644812981,-1.25949841963374,-1.03661145615814E-16));
#63061=CARTESIAN_POINT('Ctrl Pts',(2.11040940583919,-1.29643454206688,-5.55111512312578E-17));
#63062=CARTESIAN_POINT('Ctrl Pts',(2.10166865720486,-1.30772020237512,-4.0799144537779E-17));
#63063=CARTESIAN_POINT('Ctrl Pts',(2.09283023898332,-1.31893783850973,-3.98702450321844E-16));
#63064=CARTESIAN_POINT('Ctrl Pts',(2.08389831377262,-1.33008110200649,-3.88578058618805E-16));
#63065=CARTESIAN_POINT('Ctrl Pts',(2.03043260129099,-1.39678368942974,-3.27974347428123E-16));
#63066=CARTESIAN_POINT('Ctrl Pts',(1.97380215986925,-1.46059813131217,-2.08556400160018E-16));
#63067=CARTESIAN_POINT('Ctrl Pts',(1.91417150281915,-1.52123259912064,-1.11022302462516E-16));
#63068=CARTESIAN_POINT('Ctrl Pts',(1.85542332105702,-1.58096973622562,-1.49316138302572E-17));
#63069=CARTESIAN_POINT('Ctrl Pts',(1.79376241718216,-1.63762085789259,-5.35520206863283E-16));
#63070=CARTESIAN_POINT('Ctrl Pts',(1.72931881925135,-1.69086532717403,-5.55111512312578E-16));
#63071=CARTESIAN_POINT('Ctrl Pts',(1.66690919772329,-1.7424292882658,-5.74084474679515E-16));
#63072=CARTESIAN_POINT('Ctrl Pts',(1.60188918190129,-1.79079854027645,-4.05239810717764E-16));
#63073=CARTESIAN_POINT('Ctrl Pts',(1.53436012060039,-1.83563678794726,-4.44089209850063E-16));
#63074=CARTESIAN_POINT('Ctrl Pts',(1.48333459704145,-1.8695169429323,-4.73444140786276E-16));
#63075=CARTESIAN_POINT('Ctrl Pts',(1.43087616732457,-1.90138023485661,-2.26823314612322E-16));
#63076=CARTESIAN_POINT('Ctrl Pts',(1.37702479013106,-1.93106208855762,-2.22044604925031E-16));
#63077=CARTESIAN_POINT('Ctrl Pts',(0.260984867623806,2.92515103163649,15.058));
#63078=CARTESIAN_POINT('Ctrl Pts',(0.721611965671866,2.88493263312463,15.0330979289241));
#63079=CARTESIAN_POINT('Ctrl Pts',(1.17298362662806,2.74202417939443,15.0081958578483));
#63080=CARTESIAN_POINT('Ctrl Pts',(1.56185858228333,2.49936439089571,14.9832937867724));
#63081=CARTESIAN_POINT('Ctrl Pts',(2.3835871899963,1.98660190194863,14.930673416402));
#63082=CARTESIAN_POINT('Ctrl Pts',(2.92625811262771,1.02843390833919,14.8780530460316));
#63083=CARTESIAN_POINT('Ctrl Pts',(2.94584082398175,0.0600984948350938,
14.8254326756613));
#63084=CARTESIAN_POINT('Ctrl Pts',(2.96542353533579,-0.90823691866899,14.7728123052909));
#63085=CARTESIAN_POINT('Ctrl Pts',(2.46191803541247,-1.88673975206773,14.7201919349205));
#63086=CARTESIAN_POINT('Ctrl Pts',(1.6624759601657,-2.43293893833301,14.6675715645502));
#63087=CARTESIAN_POINT('Ctrl Pts',(0.863033884918936,-2.97913812459828,
14.6149511941798));
#63088=CARTESIAN_POINT('Ctrl Pts',(-0.232344765651281,-3.0930336637301,
14.5623308238094));
#63089=CARTESIAN_POINT('Ctrl Pts',(-1.12713695505886,-2.72269707033318,
14.5097104534391));
#63090=CARTESIAN_POINT('Ctrl Pts',(-2.02192914446644,-2.35236047693625,
14.4570900830687));
#63091=CARTESIAN_POINT('Ctrl Pts',(-2.71613487271139,-1.49779175101059,
14.4044697126983));
#63092=CARTESIAN_POINT('Ctrl Pts',(-2.89560267371491,-0.546185667602603,
14.351849342328));
#63093=CARTESIAN_POINT('Ctrl Pts',(-2.9293373183321,-0.367311836977727,
14.3419582672485));
#63094=CARTESIAN_POINT('Ctrl Pts',(-2.94488478294563,-0.185009395803266,
14.3320671921691));
#63095=CARTESIAN_POINT('Ctrl Pts',(-2.94325266537063,-0.0024318079996577,
14.3221761170896));
#63096=CARTESIAN_POINT('Origin',(0.,0.,-1.84858989190501));
#63097=CARTESIAN_POINT('',(-1.37702479013098,-1.93106208855768,0.));
#63098=CARTESIAN_POINT('Ctrl Pts',(-1.37994859234593,-1.93347131995891,
-1.03866568124111E-15));
#63099=CARTESIAN_POINT('Ctrl Pts',(-0.794305021574331,-2.34617453422284,
0.0482502273315914));
#63100=CARTESIAN_POINT('Ctrl Pts',(0.853330802601401,-2.62819893329841,
0.149165418329868));
#63101=CARTESIAN_POINT('Ctrl Pts',(2.68321992772198,-0.795544356782894,
0.30274557299483));
#63102=CARTESIAN_POINT('Ctrl Pts',(2.13222685489998,1.81318819272267,0.460740463994884));
#63103=CARTESIAN_POINT('Ctrl Pts',(-0.353356050373597,2.77617865909866,
0.618735354994938));
#63104=CARTESIAN_POINT('Ctrl Pts',(-2.12480812784407,1.50378450145058,0.74801849763165));
#63105=CARTESIAN_POINT('Ctrl Pts',(-2.36883710346974,0.358840951777969,
0.824636676601679));
#63106=CARTESIAN_POINT('Ctrl Pts',(-2.36806791026422,0.000580996437929554,
0.848589891905023));
#63107=CARTESIAN_POINT('Origin',(0.,0.,0.));
#63108=CARTESIAN_POINT('Ctrl Pts',(-1.03908919352511,2.13201587949043,-0.329233991005384));
#63109=CARTESIAN_POINT('Ctrl Pts',(-1.74458119175558,1.78817739379635,-0.2765690273387));
#63110=CARTESIAN_POINT('Ctrl Pts',(-2.77573338088225,0.351504794741619,
-0.171239100005331));
#63111=CARTESIAN_POINT('Ctrl Pts',(-1.80933791412281,-2.1375423700464,-0.013244209005277));
#63112=CARTESIAN_POINT('Ctrl Pts',(0.800729748594893,-2.68087948155196,
0.144750681994776));
#63113=CARTESIAN_POINT('Ctrl Pts',(2.68321992772198,-0.795544356782894,
0.30274557299483));
#63114=CARTESIAN_POINT('Ctrl Pts',(2.13222685489998,1.81318819272267,0.460740463994884));
#63115=CARTESIAN_POINT('Ctrl Pts',(-0.353356050373597,2.77617865909866,
0.618735354994938));
#63116=CARTESIAN_POINT('Ctrl Pts',(-2.51821971460423,1.2212058130903,0.77673024599499));
#63117=CARTESIAN_POINT('Ctrl Pts',(-2.39875016986203,-1.44183805604875,
0.934725136995045));
#63118=CARTESIAN_POINT('Ctrl Pts',(-0.103189861818606,-2.79677945469355,
1.0927200279951));
#63119=CARTESIAN_POINT('Ctrl Pts',(2.28595558559378,-1.6146683983646,1.25071491899515));
#63120=CARTESIAN_POINT('Ctrl Pts',(2.60139192527736,1.0322363870214,1.4087098099952));
#63121=CARTESIAN_POINT('Ctrl Pts',(0.556949311928898,2.7427217714679,1.56670470099526));
#63122=CARTESIAN_POINT('Ctrl Pts',(-1.99273057992189,1.96513605211958,1.72469959199531));
#63123=CARTESIAN_POINT('Ctrl Pts',(-2.73469173326279,-0.595142683011921,
1.88269448299537));
#63124=CARTESIAN_POINT('Ctrl Pts',(-0.995855715555496,-2.61553061219188,
2.04068937399542));
#63125=CARTESIAN_POINT('Ctrl Pts',(1.64637781974439,-2.26322161422709,2.19868426499547));
#63126=CARTESIAN_POINT('Ctrl Pts',(2.79508756969503,0.142186649832604,2.35667915599553));
#63127=CARTESIAN_POINT('Ctrl Pts',(1.40821242874264,2.41860884498944,2.51467404699558));
#63128=CARTESIAN_POINT('Ctrl Pts',(-1.25613315819632,2.50097199645567,2.67266893799564));
#63129=CARTESIAN_POINT('Ctrl Pts',(-2.78096812139655,0.314559449318749,
2.83066382899569));
#63130=CARTESIAN_POINT('Ctrl Pts',(-1.78302687496254,-2.15720801874703,
2.98865871999574));
#63131=CARTESIAN_POINT('Ctrl Pts',(0.832400628534772,-2.67204800324426,
3.1466536109958));
#63132=CARTESIAN_POINT('Ctrl Pts',(2.69270963387839,-0.762919488957052,
3.30464850199585));
#63133=CARTESIAN_POINT('Ctrl Pts',(2.11030679852043,1.83829718168443,3.4626433929959));
#63134=CARTESIAN_POINT('Ctrl Pts',(-0.386476751895552,2.77188871376435,
3.62063828399595));
#63135=CARTESIAN_POINT('Ctrl Pts',(-2.53266500493224,1.1909405067813,3.77863317499601));
#63136=CARTESIAN_POINT('Ctrl Pts',(-2.38132711099884,-1.47037835529628,
3.93662806599605));
#63137=CARTESIAN_POINT('Ctrl Pts',(-0.0697503817448946,-2.79783241149437,
4.09462295699612));
#63138=CARTESIAN_POINT('Ctrl Pts',(2.30510093209087,-1.58721170953314,4.25261784799616));
#63139=CARTESIAN_POINT('Ctrl Pts',(2.5888625630092,1.06326005653742,4.41061273899623));
#63140=CARTESIAN_POINT('Ctrl Pts',(0.524118009051023,2.74918744918107,4.56860762999628));
#63141=CARTESIAN_POINT('Ctrl Pts',(-2.01608414683087,1.9411687281004,4.72660252099633));
#63142=CARTESIAN_POINT('Ctrl Pts',(-2.72738037475851,-0.627795834204506,
4.88459741199638));
#63143=CARTESIAN_POINT('Ctrl Pts',(-0.964512940920624,-2.62725067416123,
5.04259230299644));
#63144=CARTESIAN_POINT('Ctrl Pts',(1.67331967629405,-2.24337526486265,5.20058719399648));
#63145=CARTESIAN_POINT('Ctrl Pts',(2.79318773824162,0.175594923072764,5.35858208499656));
#63146=CARTESIAN_POINT('Ctrl Pts',(1.37919449268132,2.43527285317938,5.51657697599659));
#63147=CARTESIAN_POINT('Ctrl Pts',(-1.28594543116668,2.48577466117395,5.67457186699666));
#63148=CARTESIAN_POINT('Ctrl Pts',(-2.78453026564846,0.281287251330417,
5.8325667579967));
#63149=CARTESIAN_POINT('Ctrl Pts',(-1.75710748413146,-2.17837200846936,
5.99056164899676));
#63150=CARTESIAN_POINT('Ctrl Pts',(0.864288593995119,-2.66190468356086,
6.14855653999681));
#63151=CARTESIAN_POINT('Ctrl Pts',(2.70163876039796,-0.730670463607777,
6.30655143099686));
#63152=CARTESIAN_POINT('Ctrl Pts',(2.08817696449889,1.86339697407977,6.46454632199692));
#63153=CARTESIAN_POINT('Ctrl Pts',(-0.419590302218696,2.76706980330411,
6.62254121299697));
#63154=CARTESIAN_POINT('Ctrl Pts',(-2.54672306405081,1.16057440653543,6.78053610399702));
#63155=CARTESIAN_POINT('Ctrl Pts',(-2.3635768050391,-1.49874480975067,6.93853099499709));
#63156=CARTESIAN_POINT('Ctrl Pts',(-0.0362940343214689,-2.79846637663312,
7.09652588599712));
#63157=CARTESIAN_POINT('Ctrl Pts',(2.32391314315961,-1.55953807940794,7.2545207769972));
#63158=CARTESIAN_POINT('Ctrl Pts',(2.57596499873257,1.09413693995685,7.41251566799723));
#63159=CARTESIAN_POINT('Ctrl Pts',(0.491210792034311,2.75525738831465,7.5705105589973));
#63160=CARTESIAN_POINT('Ctrl Pts',(-2.03914898665099,1.91692533196097,7.72850544999735));
#63161=CARTESIAN_POINT('Ctrl Pts',(-2.71967939412015,-0.66035998612245,
7.8865003409974));
#63162=CARTESIAN_POINT('Ctrl Pts',(-0.9330321424437,-2.63859476601473,8.04449523199746));
#63163=CARTESIAN_POINT('Ctrl Pts',(1.70002224901497,-2.22320841823872,8.2024901229975));
#63164=CARTESIAN_POINT('Ctrl Pts',(2.79088864512093,0.208978201275766,8.36048501399757));
#63165=CARTESIAN_POINT('Ctrl Pts',(1.34997937336987,2.45158867054595,8.51847990499762));
#63166=CARTESIAN_POINT('Ctrl Pts',(-1.31557386100644,2.47022200101732,8.67647479599767));
#63167=CARTESIAN_POINT('Ctrl Pts',(-2.78769435259396,0.247974826523285,
8.83446968699772));
#63168=CARTESIAN_POINT('Ctrl Pts',(-1.73093690286391,-2.19922458070505,
8.99246457799778));
#63169=CARTESIAN_POINT('Ctrl Pts',(0.896053003445084,-2.6513808351669,9.15045946899784));
#63170=CARTESIAN_POINT('Ctrl Pts',(2.71018167460651,-0.698316982967359,
9.30845435999788));
#63171=CARTESIAN_POINT('Ctrl Pts',(2.06574861445826,1.88823038317285,9.46644925099794));
#63172=CARTESIAN_POINT('Ctrl Pts',(-0.45264386973844,2.76185532663481,9.62444414199799));
#63173=CARTESIAN_POINT('Ctrl Pts',(-2.5604170561675,1.13004239591331,9.78243903299804));
#63174=CARTESIAN_POINT('Ctrl Pts',(-2.34548861359897,-1.52689701078686,
9.9404339239981));
#63175=CARTESIAN_POINT('Ctrl Pts',(-0.00283249851198579,-2.79870028674429,
10.0984288149982));
#63176=CARTESIAN_POINT('Ctrl Pts',(2.34239313895008,-1.53164150527581,10.2564237059982));
#63177=CARTESIAN_POINT('Ctrl Pts',(2.56269918704329,1.12485741087042,10.4144185969983));
#63178=CARTESIAN_POINT('Ctrl Pts',(0.458233353927178,2.76093344928963,10.5724134879983));
#63179=CARTESIAN_POINT('Ctrl Pts',(-2.06192231968409,1.89240790151988,10.7304083789984));
#63180=CARTESIAN_POINT('Ctrl Pts',(-2.71158962134898,-0.692829736205835,
10.8884032699984));
#63181=CARTESIAN_POINT('Ctrl Pts',(-0.90141796228012,-2.64956165719617,
11.0463981609985));
#63182=CARTESIAN_POINT('Ctrl Pts',(1.72648179491819,-2.20272375262492,11.2043930519985));
#63183=CARTESIAN_POINT('Ctrl Pts',(2.7881905800153,0.242331605070017,11.3623879429986));
#63184=CARTESIAN_POINT('Ctrl Pts',(1.32057126786748,2.46755402056041,11.5203828339987));
#63185=CARTESIAN_POINT('Ctrl Pts',(-1.34501422335496,2.45431621031658,11.6783777249987));
#63186=CARTESIAN_POINT('Ctrl Pts',(-2.79045992331823,0.214626951768239,
11.8363726159988));
#63187=CARTESIAN_POINT('Ctrl Pts',(-1.70451887724915,-2.21976276122321,
11.9943675069988));
#63188=CARTESIAN_POINT('Ctrl Pts',(0.927689321261817,-2.64047796075702,
12.1523623979988));
#63189=CARTESIAN_POINT('Ctrl Pts',(2.71833714731268,-0.66586366962402,12.3103572889989));
#63190=CARTESIAN_POINT('Ctrl Pts',(2.04302496870488,1.91279385105346,12.468352179999));
#63191=CARTESIAN_POINT('Ctrl Pts',(-0.48563275555883,2.75624604578475,12.626347070999));
#63192=CARTESIAN_POINT('Ctrl Pts',(-2.57374497374716,1.09934880708429,12.7843419619991));
#63193=CARTESIAN_POINT('Ctrl Pts',(-2.32706521767492,-1.55483087129818,
12.9423368529991));
#63194=CARTESIAN_POINT('Ctrl Pts',(0.0306296239850783,-2.7985342282319,
13.1003317439992));
#63195=CARTESIAN_POINT('Ctrl Pts',(2.36053793034993,-1.50352574600393,13.2583266349992));
#63196=CARTESIAN_POINT('Ctrl Pts',(2.54906768788899,1.15541663986578,13.4163215259993));
#63197=CARTESIAN_POINT('Ctrl Pts',(0.42518914129335,2.76621565710669,13.5743164169993));
#63198=CARTESIAN_POINT('Ctrl Pts',(-2.08439846825039,1.86761834358563,13.7323113079994));
#63199=CARTESIAN_POINT('Ctrl Pts',(-2.7031168406022,-0.725197389434075,
13.8903061989994));
#63200=CARTESIAN_POINT('Ctrl Pts',(-0.869666078203209,-2.66015561356989,
14.0483010899995));
#63201=CARTESIAN_POINT('Ctrl Pts',(1.75267763866885,-2.18191305067097,14.2062959809995));
#63202=CARTESIAN_POINT('Ctrl Pts',(2.78512620401791,0.275629071355557,14.3642908719996));
#63203=CARTESIAN_POINT('Ctrl Pts',(1.29091271455523,2.48320730756548,14.5222857629997));
#63204=CARTESIAN_POINT('Ctrl Pts',(-1.37414448785656,2.43798182357128,14.6802806539997));
#63205=CARTESIAN_POINT('Ctrl Pts',(-2.79305172314729,0.181396953694044,
14.8382755449998));
#63206=CARTESIAN_POINT('Ctrl Pts',(-1.67742675687761,-2.24026772494819,
14.9962704359998));
#63207=CARTESIAN_POINT('Ctrl Pts',(0.958368222991996,-2.62865236842956,
15.1542653269999));
#63208=CARTESIAN_POINT('Ctrl Pts',(2.7277014223945,-0.634378452891388,15.3122602179999));
#63209=CARTESIAN_POINT('Ctrl Pts',(2.01676643438217,1.93930517753648,15.470255109));
#63210=CARTESIAN_POINT('Ctrl Pts',(0.331786659212352,2.47609764328476,15.5755850363333));
#63211=CARTESIAN_POINT('Ctrl Pts',(-0.439445221994538,2.33068358199181,
15.62825));
#63212=CARTESIAN_POINT('Ctrl Pts',(-1.12236674703448,2.30288577939268,-0.219489327336923));
#63213=CARTESIAN_POINT('Ctrl Pts',(-1.88440023178909,1.93149044095738,-0.166824363670239));
#63214=CARTESIAN_POINT('Ctrl Pts',(-2.99819386511655,0.37967606197771,-0.0614944363368692));
#63215=CARTESIAN_POINT('Ctrl Pts',(-1.9543468660962,-2.30885518920509,0.096500454663184));
#63216=CARTESIAN_POINT('Ctrl Pts',(0.864904041716857,-2.89573792283723,
0.254495345663238));
#63217=CARTESIAN_POINT('Ctrl Pts',(2.89826594350265,-0.859303067925248,
0.412490236663291));
#63218=CARTESIAN_POINT('Ctrl Pts',(2.30311366337569,1.95850572434841,0.570485127663346));
#63219=CARTESIAN_POINT('Ctrl Pts',(-0.381675686047029,2.99867483004853,
0.728480018663398));
#63220=CARTESIAN_POINT('Ctrl Pts',(-2.72004182798788,1.31907905927489,0.886474909663454));
#63221=CARTESIAN_POINT('Ctrl Pts',(-2.59099742531531,-1.55739382028214,
1.0444698006635));
#63222=CARTESIAN_POINT('Ctrl Pts',(-0.111459988476451,-3.02092667145178,
1.20246469166356));
#63223=CARTESIAN_POINT('Ctrl Pts',(2.46916294621846,-1.74407560881646,1.36045958266361));
#63224=CARTESIAN_POINT('Ctrl Pts',(2.80987985548213,1.11496472400166,1.51845447366367));
#63225=CARTESIAN_POINT('Ctrl Pts',(0.60158588058462,2.96253654820512,1.67644936466372));
#63226=CARTESIAN_POINT('Ctrl Pts',(-2.15243749298894,2.12263140839256,1.83444425566377));
#63227=CARTESIAN_POINT('Ctrl Pts',(-2.95386294451934,-0.642840250207365,
1.99243914666383));
#63228=CARTESIAN_POINT('Ctrl Pts',(-1.07566833237088,-2.82515168405898,
2.15043403766388));
#63229=CARTESIAN_POINT('Ctrl Pts',(1.77832637414643,-2.44460696618424,2.30842892866393));
#63230=CARTESIAN_POINT('Ctrl Pts',(3.01909919073696,0.153582164686878,2.46642381966399));
#63231=CARTESIAN_POINT('Ctrl Pts',(1.52107327516274,2.61244766918467,2.62441871066404));
#63232=CARTESIAN_POINT('Ctrl Pts',(-1.35680564805421,2.70141179561648,2.7824136016641));
#63233=CARTESIAN_POINT('Ctrl Pts',(-3.00384814265038,0.339769740731444,
2.94040849266415));
#63234=CARTESIAN_POINT('Ctrl Pts',(-1.92592713503036,-2.33009693659115,
3.0984033836642));
#63235=CARTESIAN_POINT('Ctrl Pts',(0.899113176712534,-2.88619864782458,
3.25639827466426));
#63236=CARTESIAN_POINT('Ctrl Pts',(2.90851619987664,-0.824063487913928,
3.41439316566431));
#63237=CARTESIAN_POINT('Ctrl Pts',(2.27943682934948,1.98562706719167,3.57238805666436));
#63238=CARTESIAN_POINT('Ctrl Pts',(-0.417450838226782,2.99404106807715,
3.73038294766441));
#63239=CARTESIAN_POINT('Ctrl Pts',(-2.73564483263507,1.2863881472707,3.88837783866447));
#63240=CARTESIAN_POINT('Ctrl Pts',(-2.57217799958985,-1.5882214749488,4.04637272966452));
#63241=CARTESIAN_POINT('Ctrl Pts',(-0.0753405093145775,-3.02206401722216,
4.20436762066458));
#63242=CARTESIAN_POINT('Ctrl Pts',(2.48984269190601,-1.71441841026206,4.36236251166463));
#63243=CARTESIAN_POINT('Ctrl Pts',(2.79634633048836,1.1484747780497,4.52035740266469));
#63244=CARTESIAN_POINT('Ctrl Pts',(0.566123320833673,2.9695204161036,4.67835229366474));
#63245=CARTESIAN_POINT('Ctrl Pts',(-2.1776627259012,2.09674322895411,4.83634718466479));
#63246=CARTESIAN_POINT('Ctrl Pts',(-2.94596561894615,-0.678110380349046,
4.99434207566485));
#63247=CARTESIAN_POINT('Ctrl Pts',(-1.04181359860098,-2.83781104757613,
5.1523369666649));
#63248=CARTESIAN_POINT('Ctrl Pts',(1.80742747930962,-2.42317003592312,5.31033185766495));
#63249=CARTESIAN_POINT('Ctrl Pts',(3.01704709774863,0.189667935951029,5.46832674866501));
#63250=CARTESIAN_POINT('Ctrl Pts',(1.48972970359473,2.63044721030322,5.62632163966506));
#63251=CARTESIAN_POINT('Ctrl Pts',(-1.38900721847178,2.68499647355363,5.78431653066512));
#63252=CARTESIAN_POINT('Ctrl Pts',(-3.00769577409666,0.303830950437453,
5.94231142166516));
#63253=CARTESIAN_POINT('Ctrl Pts',(-1.89793044085485,-2.35295710917974,
6.10030631266523));
#63254=CARTESIAN_POINT('Ctrl Pts',(0.933556795495496,-2.87524239422467,
6.25830120366527));
#63255=CARTESIAN_POINT('Ctrl Pts',(2.91816094909363,-0.789229872184075,
6.41629609466533));
#63256=CARTESIAN_POINT('Ctrl Pts',(2.25553340510261,2.01273847641193,6.57429098566538));
#63257=CARTESIAN_POINT('Ctrl Pts',(-0.453218266076613,2.98883594719704,
6.73228587666544));
#63258=CARTESIAN_POINT('Ctrl Pts',(-2.75082957152067,1.25358836322381,6.89028076766548));
#63259=CARTESIAN_POINT('Ctrl Pts',(-2.55300509962799,-1.61886135207317,
7.04827565866555));
#63260=CARTESIAN_POINT('Ctrl Pts',(-0.0392028109733089,-3.02274879134448,
7.20627054966559));
#63261=CARTESIAN_POINT('Ctrl Pts',(2.51016260310644,-1.68452688370611,7.36426544066566));
#63262=CARTESIAN_POINT('Ctrl Pts',(2.78241509402469,1.18182628186475,7.5222603316657));
#63263=CARTESIAN_POINT('Ctrl Pts',(0.530578762823495,2.97607682904918,7.68025522266576));
#63264=CARTESIAN_POINT('Ctrl Pts',(-2.2025760917615,2.07055685166173,7.83825011366581));
#63265=CARTESIAN_POINT('Ctrl Pts',(-2.93764744506665,-0.713284378390626,
7.99624500466586));
#63266=CARTESIAN_POINT('Ctrl Pts',(-1.0078097791014,-2.85006430894292,8.15423989566592));
#63267=CARTESIAN_POINT('Ctrl Pts',(1.83627012329917,-2.40138692222673,8.31223478666596));
#63268=CARTESIAN_POINT('Ctrl Pts',(3.01456374436274,0.225726708956776,8.47022967766603));
#63269=CARTESIAN_POINT('Ctrl Pts',(1.45817314557243,2.64807065492862,8.62822456866608));
#63270=CARTESIAN_POINT('Ctrl Pts',(-1.42101021169528,2.66819734918923,8.78621945966612));
#63271=CARTESIAN_POINT('Ctrl Pts',(-3.01111344602942,0.267848709355943,
8.9442143506662));
#63272=CARTESIAN_POINT('Ctrl Pts',(-1.86966242464576,-2.37548090580212,
9.10220924166623));
#63273=CARTESIAN_POINT('Ctrl Pts',(0.967866955901341,-2.86387511453221,
9.26020413266631));
#63274=CARTESIAN_POINT('Ctrl Pts',(2.92738853310682,-0.754283429618888,
9.41819902366633));
#63275=CARTESIAN_POINT('Ctrl Pts',(2.23130754034209,2.03956215310421,9.57619391466641));
#63276=CARTESIAN_POINT('Ctrl Pts',(-0.488920903815691,2.98320355754919,
9.73418880566644));
#63277=CARTESIAN_POINT('Ctrl Pts',(-2.76562106534208,1.22060937195346,9.89218369666651));
#63278=CARTESIAN_POINT('Ctrl Pts',(-2.53346723443519,-1.64926980449067,
10.0501785876666));
#63279=CARTESIAN_POINT('Ctrl Pts',(-0.00305950842402692,-3.02300144812525,
10.2081734786666));
#63280=CARTESIAN_POINT('Ctrl Pts',(2.53012367371502,-1.65439454534941,10.3661683696667));
#63281=CARTESIAN_POINT('Ctrl Pts',(2.76808609704807,1.21500883753128,10.5241632606667));
#63282=CARTESIAN_POINT('Ctrl Pts',(0.494958355870487,2.98220779656589,10.6821581516668));
#63283=CARTESIAN_POINT('Ctrl Pts',(-2.22717458809345,2.0440744776545,10.8401530426668));
#63284=CARTESIAN_POINT('Ctrl Pts',(-2.92890931940236,-0.748356408785326,
10.9981479336669));
#63285=CARTESIAN_POINT('Ctrl Pts',(-0.973661888071959,-2.86191013898051,
11.1561428246669));
#63286=CARTESIAN_POINT('Ctrl Pts',(1.86485026314516,-2.37926051801397,11.314137715667));
#63287=CARTESIAN_POINT('Ctrl Pts',(3.01164944347811,0.261753213276476,11.472132606667));
#63288=CARTESIAN_POINT('Ctrl Pts',(1.42640813452734,2.66531554408024,11.6301274976671));
#63289=CARTESIAN_POINT('Ctrl Pts',(-1.45281006480367,2.6510167927182,11.7881223886671));
#63290=CARTESIAN_POINT('Ctrl Pts',(-3.01410066275426,0.231828177198969,
11.9461172796672));
#63291=CARTESIAN_POINT('Ctrl Pts',(-1.84112713272175,-2.39766511385838,
12.1041121706673));
#63292=CARTESIAN_POINT('Ctrl Pts',(1.00203875880082,-2.85209843187493,12.2621070616673));
#63293=CARTESIAN_POINT('Ctrl Pts',(2.9361976242116,-0.71922915328282,12.4201019526674));
#63294=CARTESIAN_POINT('Ctrl Pts',(2.20676271346495,2.0660942542105,12.5780968436674));
#63295=CARTESIAN_POINT('Ctrl Pts',(-0.52455367595618,2.97714472223446,12.7360917346675));
#63296=CARTESIAN_POINT('Ctrl Pts',(-2.78001714567073,1.1874558528297,12.8940866256675));
#63297=CARTESIAN_POINT('Ctrl Pts',(-2.51356729987571,-1.67944241753446,
13.0520815166676));
#63298=CARTESIAN_POINT('Ctrl Pts',(0.0330844278327718,-3.02282208089334,
13.2100764076676));
#63299=CARTESIAN_POINT('Ctrl Pts',(2.5497226750577,-1.62402545531265,13.3680712986677));
#63300=CARTESIAN_POINT('Ctrl Pts',(2.75336210467249,1.24801722858484,13.5260661896677));
#63301=CARTESIAN_POINT('Ctrl Pts',(0.459265822762407,2.98791334565805,13.6840610806678));
#63302=CARTESIAN_POINT('Ctrl Pts',(-2.25145208218098,2.01729816656161,13.8420559716679));
#63303=CARTESIAN_POINT('Ctrl Pts',(-2.91975748968037,-0.78331815979697,
14.0000508626679));
#63304=CARTESIAN_POINT('Ctrl Pts',(-0.939365256882179,-2.87335314543991,
14.158045753668));
#63305=CARTESIAN_POINT('Ctrl Pts',(1.893145566493,-2.35678194735699,14.316040644668));
#63306=CARTESIAN_POINT('Ctrl Pts',(3.0083394738034,0.297719296989276,14.4740355356681));
#63307=CARTESIAN_POINT('Ctrl Pts',(1.3943726035929,2.68222336000765,14.6320304266681));
#63308=CARTESIAN_POINT('Ctrl Pts',(-1.4842749673478,2.63337329047569,14.7900253176682));
#63309=CARTESIAN_POINT('Ctrl Pts',(-3.01690018175728,0.195934968921086,
14.9480202086682));
#63310=CARTESIAN_POINT('Ctrl Pts',(-1.81186372087882,-2.41981344296957,
15.1060150996683));
#63311=CARTESIAN_POINT('Ctrl Pts',(1.03517641373175,-2.8393250802945,15.2640099906683));
#63312=CARTESIAN_POINT('Ctrl Pts',(2.94631239686769,-0.685220561427491,
15.4220048816684));
#63313=CARTESIAN_POINT('Ctrl Pts',(2.17839969522424,2.09473032457841,15.5799997726684));
#63314=CARTESIAN_POINT('Ctrl Pts',(0.358377621218746,2.67454389339306,15.6853297000018));
#63315=CARTESIAN_POINT('Ctrl Pts',(-0.474664453622694,2.51747565713054,
15.7379946636685));
#63316=CARTESIAN_POINT('Ctrl Pts',(-1.20564430054385,2.47375567929493,-0.109744663668462));
#63317=CARTESIAN_POINT('Ctrl Pts',(-2.02421927182262,2.0748034881184,-0.057079700001777));
#63318=CARTESIAN_POINT('Ctrl Pts',(-3.22065434935084,0.407847329213798,
0.0482502273315919));
#63319=CARTESIAN_POINT('Ctrl Pts',(-2.09935581806959,-2.48016800836378,
0.206245118331646));
#63320=CARTESIAN_POINT('Ctrl Pts',(0.929078334838823,-3.11059636412251,
0.364240009331699));
#63321=CARTESIAN_POINT('Ctrl Pts',(3.11331195928332,-0.923061779067598,
0.522234900331752));
#63322=CARTESIAN_POINT('Ctrl Pts',(2.4740004718514,2.10382325597413,0.680229791331807));
#63323=CARTESIAN_POINT('Ctrl Pts',(-0.409995321720456,3.2211710009984,0.83822468233186));
#63324=CARTESIAN_POINT('Ctrl Pts',(-2.92186394137152,1.41695230545948,0.996219573331913));
#63325=CARTESIAN_POINT('Ctrl Pts',(-2.78324468076858,-1.67294958451553,
1.15421446433197));
#63326=CARTESIAN_POINT('Ctrl Pts',(-0.119730115134298,-3.24507388821001,
1.31220935533202));
#63327=CARTESIAN_POINT('Ctrl Pts',(2.65237030684314,-1.87348281926831,1.47020424633207));
#63328=CARTESIAN_POINT('Ctrl Pts',(3.0183677856869,1.19769306098192,1.62819913733213));
#63329=CARTESIAN_POINT('Ctrl Pts',(0.646222449240343,3.18235132494235,1.78619402833218));
#63330=CARTESIAN_POINT('Ctrl Pts',(-2.31214440605599,2.28012676466554,1.94418891933223));
#63331=CARTESIAN_POINT('Ctrl Pts',(-3.17303415577589,-0.690537817402807,
2.10218381033229));
#63332=CARTESIAN_POINT('Ctrl Pts',(-1.15548094918627,-3.03477275592607,
2.26017870133234));
#63333=CARTESIAN_POINT('Ctrl Pts',(1.91027492854846,-2.62599231814139,2.4181735923324));
#63334=CARTESIAN_POINT('Ctrl Pts',(3.24311081177889,0.16497767954115,2.57616848333245));
#63335=CARTESIAN_POINT('Ctrl Pts',(1.63393412158284,2.80628649337991,2.7341633743325));
#63336=CARTESIAN_POINT('Ctrl Pts',(-1.45747813791209,2.90185159477728,2.89215826533256));
#63337=CARTESIAN_POINT('Ctrl Pts',(-3.22672816390422,0.364980032144142,
3.05015315633261));
#63338=CARTESIAN_POINT('Ctrl Pts',(-2.06882739509817,-2.50298585443527,
3.20814804733266));
#63339=CARTESIAN_POINT('Ctrl Pts',(0.965825724890286,-3.10034929240489,
3.36614293833272));
#63340=CARTESIAN_POINT('Ctrl Pts',(3.1243227658749,-0.885207486870811,3.52413782933277));
#63341=CARTESIAN_POINT('Ctrl Pts',(2.44856686017853,2.13295695269892,3.68213272033283));
#63342=CARTESIAN_POINT('Ctrl Pts',(-0.448424924558006,3.21619342238995,
3.84012761133287));
#63343=CARTESIAN_POINT('Ctrl Pts',(-2.9386246603379,1.3818357877601,3.99812250233293));
#63344=CARTESIAN_POINT('Ctrl Pts',(-2.76302888818086,-1.70606459460131,
4.15611739333298));
#63345=CARTESIAN_POINT('Ctrl Pts',(-0.0809306368842651,-3.24629562294995,
4.31411228433304));
#63346=CARTESIAN_POINT('Ctrl Pts',(2.67458445172116,-1.84162511099097,4.47210717533309));
#63347=CARTESIAN_POINT('Ctrl Pts',(3.00383009796752,1.23368949956199,4.63010206633314));
#63348=CARTESIAN_POINT('Ctrl Pts',(0.608128632616327,3.18985338302612,4.7880969573332));
#63349=CARTESIAN_POINT('Ctrl Pts',(-2.33924130497153,2.25231772980782,4.94609184833325));
#63350=CARTESIAN_POINT('Ctrl Pts',(-3.16455086313379,-0.728424926493586,
5.10408673933331));
#63351=CARTESIAN_POINT('Ctrl Pts',(-1.11911425628133,-3.04837142099104,
5.26208163033336));
#63352=CARTESIAN_POINT('Ctrl Pts',(1.94153528232519,-2.60296480698359,5.42007652133342));
#63353=CARTESIAN_POINT('Ctrl Pts',(3.24090645725565,0.20374094882929,5.57807141233347));
#63354=CARTESIAN_POINT('Ctrl Pts',(1.60026491450814,2.82562156742707,5.73606630333352));
#63355=CARTESIAN_POINT('Ctrl Pts',(-1.49206900577688,2.8842182859333,5.89406119433358));
#63356=CARTESIAN_POINT('Ctrl Pts',(-3.23086128254485,0.326374649544494,
6.05205608533362));
#63357=CARTESIAN_POINT('Ctrl Pts',(-2.03875339757824,-2.52754220989012,
6.21005097633369));
#63358=CARTESIAN_POINT('Ctrl Pts',(1.00282499699587,-3.08858010488847,6.36804586733373));
#63359=CARTESIAN_POINT('Ctrl Pts',(3.1346831377893,-0.847789280760374,6.52604075833379));
#63360=CARTESIAN_POINT('Ctrl Pts',(2.42288984570632,2.16207997874408,6.68403564933384));
#63361=CARTESIAN_POINT('Ctrl Pts',(-0.486846229934527,3.21060209108997,
6.8420305403339));
#63362=CARTESIAN_POINT('Ctrl Pts',(-2.95493607899053,1.34660231991219,7.00002543133394));
#63363=CARTESIAN_POINT('Ctrl Pts',(-2.74243339421689,-1.73897789439567,
7.15802032233401));
#63364=CARTESIAN_POINT('Ctrl Pts',(-0.042111587625147,-3.24703120605584,
7.31601521333405));
#63365=CARTESIAN_POINT('Ctrl Pts',(2.69641206305327,-1.80951568800428,7.47401010433411));
#63366=CARTESIAN_POINT('Ctrl Pts',(2.98886518931682,1.26951562377266,7.63200499533417));
#63367=CARTESIAN_POINT('Ctrl Pts',(0.56994673361268,3.19689626978371,7.78999988633422));
#63368=CARTESIAN_POINT('Ctrl Pts',(-2.36600319687202,2.2241883713625,7.94799477733426));
#63369=CARTESIAN_POINT('Ctrl Pts',(-3.15561549601314,-0.766208770658805,
8.10598966833433));
#63370=CARTESIAN_POINT('Ctrl Pts',(-1.0825874157591,-3.06153385187112,8.26398455933438));
#63371=CARTESIAN_POINT('Ctrl Pts',(1.97251799758337,-2.57956542621475,8.42197945033443));
#63372=CARTESIAN_POINT('Ctrl Pts',(3.23823884360454,0.242475216637791,8.57997434133449));
#63373=CARTESIAN_POINT('Ctrl Pts',(1.566366917775,2.84455263931128,8.73796923233454));
#63374=CARTESIAN_POINT('Ctrl Pts',(-1.52644656238412,2.86617269736115,8.89596412333459));
#63375=CARTESIAN_POINT('Ctrl Pts',(-3.23453253946489,0.287722592188601,
9.05395901433465));
#63376=CARTESIAN_POINT('Ctrl Pts',(-2.0083879464276,-2.55173723089919,9.21195390533469));
#63377=CARTESIAN_POINT('Ctrl Pts',(1.0396809083576,-3.07636939389751,9.36994879633477));
#63378=CARTESIAN_POINT('Ctrl Pts',(3.14459539160713,-0.810249876270418,
9.5279436873348));
#63379=CARTESIAN_POINT('Ctrl Pts',(2.39686646622593,2.19089392303558,9.68593857833487));
#63380=CARTESIAN_POINT('Ctrl Pts',(-0.525197937892946,3.20455178846357,
9.8439334693349));
#63381=CARTESIAN_POINT('Ctrl Pts',(-2.97082507451666,1.31117634799362,10.001928360335));
#63382=CARTESIAN_POINT('Ctrl Pts',(-2.72144585527141,-1.77164259819448,
10.159923251335));
#63383=CARTESIAN_POINT('Ctrl Pts',(-0.00328651833606387,-3.24730260950622,
10.3179181423351));
#63384=CARTESIAN_POINT('Ctrl Pts',(2.71785420847995,-1.77714758542301,10.4759130333351));
#63385=CARTESIAN_POINT('Ctrl Pts',(2.97347300705285,1.30516026419214,10.6339079243352));
#63386=CARTESIAN_POINT('Ctrl Pts',(0.531683357813799,3.20348214384215,10.7919028153352));
#63387=CARTESIAN_POINT('Ctrl Pts',(-2.39242685650282,2.19574105378912,10.9498977063353));
#63388=CARTESIAN_POINT('Ctrl Pts',(-3.14622901745573,-0.803883081364814,
11.1078925973353));
#63389=CARTESIAN_POINT('Ctrl Pts',(-1.0459058138638,-3.07425862076485,11.2658874883354));
#63390=CARTESIAN_POINT('Ctrl Pts',(2.00321873137213,-2.55579728340303,11.4238823793354));
#63391=CARTESIAN_POINT('Ctrl Pts',(3.23510830694092,0.281174821482934,11.5818772703355));
#63392=CARTESIAN_POINT('Ctrl Pts',(1.5322450011872,2.86307706760007,11.7398721613356));
#63393=CARTESIAN_POINT('Ctrl Pts',(-1.56060590625239,2.84771737511982,11.8978670523356));
#63394=CARTESIAN_POINT('Ctrl Pts',(-3.23774140219028,0.2490294026297,12.0558619433357));
#63395=CARTESIAN_POINT('Ctrl Pts',(-1.97773538819436,-2.57556746649356,
12.2138568343357));
#63396=CARTESIAN_POINT('Ctrl Pts',(1.07638819633982,-3.06371890299285,12.3718517253358));
#63397=CARTESIAN_POINT('Ctrl Pts',(3.15405810111051,-0.772594636941618,
12.5298466163358));
#63398=CARTESIAN_POINT('Ctrl Pts',(2.37050045822502,2.21939465736754,12.6878415073359));
#63399=CARTESIAN_POINT('Ctrl Pts',(-0.563474596353531,3.19804339868417,
12.8458363983359));
#63400=CARTESIAN_POINT('Ctrl Pts',(-2.98628931759431,1.2755628985751,13.003831289336));
#63401=CARTESIAN_POINT('Ctrl Pts',(-2.70006938207651,-1.80405396377073,
13.161826180336));
#63402=CARTESIAN_POINT('Ctrl Pts',(0.0355392316804697,-3.24710993355476,
13.3198210713361));
#63403=CARTESIAN_POINT('Ctrl Pts',(2.73890741976546,-1.74452516462138,13.4778159623361));
#63404=CARTESIAN_POINT('Ctrl Pts',(2.95765652145599,1.3406178173039,13.6358108533362));
#63405=CARTESIAN_POINT('Ctrl Pts',(0.493342504231463,3.20961103420941,13.7938057443362));
#63406=CARTESIAN_POINT('Ctrl Pts',(-2.41850569611158,2.16697798953759,13.9518006353363));
#63407=CARTESIAN_POINT('Ctrl Pts',(-3.13639813875855,-0.841438930159867,
14.1097955263364));
#63408=CARTESIAN_POINT('Ctrl Pts',(-1.00906443556115,-3.08655067730993,
14.2677904173364));
#63409=CARTESIAN_POINT('Ctrl Pts',(2.03361349431715,-2.53165084404301,14.4257853083365));
#63410=CARTESIAN_POINT('Ctrl Pts',(3.23155274358889,0.319809522622996,14.5837801993365));
#63411=CARTESIAN_POINT('Ctrl Pts',(1.49783249263057,2.88123941244982,14.7417750903366));
#63412=CARTESIAN_POINT('Ctrl Pts',(-1.59440544683904,2.8287647573801,14.8997699813366));
#63413=CARTESIAN_POINT('Ctrl Pts',(-3.24074864036727,0.210472984148126,
15.0577648723367));
#63414=CARTESIAN_POINT('Ctrl Pts',(-1.94630068488002,-2.59935916099094,
15.2157597633367));
#63415=CARTESIAN_POINT('Ctrl Pts',(1.1119846044715,-3.04999779215944,15.3737546543368));
#63416=CARTESIAN_POINT('Ctrl Pts',(3.16492337134089,-0.73606266996359,15.5317495453368));
#63417=CARTESIAN_POINT('Ctrl Pts',(2.34003295606631,2.25015547162033,15.6897444363369));
#63418=CARTESIAN_POINT('Ctrl Pts',(0.384968583225142,2.87299014350137,15.7950743636703));
#63419=CARTESIAN_POINT('Ctrl Pts',(-0.50988368525085,2.70426773226927,15.847739327337));
#63420=CARTESIAN_POINT('Ctrl Pts',(-1.28892185405322,2.64462557919718,-2.77555756156289E-16));
#63421=CARTESIAN_POINT('Ctrl Pts',(-2.16403831185614,2.21811653527943,0.0526649636666843));
#63422=CARTESIAN_POINT('Ctrl Pts',(-3.44311483358514,0.436018596449888,
0.157994891000053));
#63423=CARTESIAN_POINT('Ctrl Pts',(-2.24436477004298,-2.65148082752247,
0.315989782000107));
#63424=CARTESIAN_POINT('Ctrl Pts',(0.99325262796079,-3.32545480540779,0.47398467300016));
#63425=CARTESIAN_POINT('Ctrl Pts',(3.32835797506399,-0.986820490209951,
0.631979564000214));
#63426=CARTESIAN_POINT('Ctrl Pts',(2.64488728032712,2.24914078759987,0.789974455000268));
#63427=CARTESIAN_POINT('Ctrl Pts',(-0.438314957393884,3.44366717194826,
0.947969346000321));
#63428=CARTESIAN_POINT('Ctrl Pts',(-3.12368605475517,1.51482555164407,1.10596423700038));
#63429=CARTESIAN_POINT('Ctrl Pts',(-2.97549193622185,-1.78850534874892,
1.26395912800043));
#63430=CARTESIAN_POINT('Ctrl Pts',(-0.128000241792142,-3.46922110496824,
1.42195401900048));
#63431=CARTESIAN_POINT('Ctrl Pts',(2.83557766746782,-2.00289002972017,1.57994891000054));
#63432=CARTESIAN_POINT('Ctrl Pts',(3.22685571589167,1.28042139796218,1.73794380100059));
#63433=CARTESIAN_POINT('Ctrl Pts',(0.690859017896064,3.40216610167957,1.89593869200064));
#63434=CARTESIAN_POINT('Ctrl Pts',(-2.47185131912304,2.43762212093852,2.0539335830007));
#63435=CARTESIAN_POINT('Ctrl Pts',(-3.39220536703243,-0.738235384598252,
2.21192847400075));
#63436=CARTESIAN_POINT('Ctrl Pts',(-1.23529356600166,-3.24439382779317,
2.3699233650008));
#63437=CARTESIAN_POINT('Ctrl Pts',(2.0422234829505,-2.80737767009854,2.52791825600086));
#63438=CARTESIAN_POINT('Ctrl Pts',(3.46712243282082,0.176373194395425,2.68591314700091));
#63439=CARTESIAN_POINT('Ctrl Pts',(1.74679496800295,3.00012531757514,2.84390803800096));
#63440=CARTESIAN_POINT('Ctrl Pts',(-1.55815062776997,3.10229139393809,3.00190292900102));
#63441=CARTESIAN_POINT('Ctrl Pts',(-3.44960818515806,0.390190323556838,
3.15989782000107));
#63442=CARTESIAN_POINT('Ctrl Pts',(-2.21172765516599,-2.67587477227939,
3.31789271100113));
#63443=CARTESIAN_POINT('Ctrl Pts',(1.03253827306805,-3.31449993698521,3.47588760200118));
#63444=CARTESIAN_POINT('Ctrl Pts',(3.34012933187316,-0.946351485827688,
3.63388249300123));
#63445=CARTESIAN_POINT('Ctrl Pts',(2.61769689100758,2.28028683820616,3.79187738400129));
#63446=CARTESIAN_POINT('Ctrl Pts',(-0.479399010889233,3.43834577670275,
3.94987227500134));
#63447=CARTESIAN_POINT('Ctrl Pts',(-3.14160448804072,1.4772834282495,4.1078671660014));
#63448=CARTESIAN_POINT('Ctrl Pts',(-2.95387977677187,-1.82390771425382,
4.26586205700145));
#63449=CARTESIAN_POINT('Ctrl Pts',(-0.0865207644539496,-3.47052722867774,
4.4238569480015));
#63450=CARTESIAN_POINT('Ctrl Pts',(2.85932621153631,-1.96883181171989,4.58185183900155));
#63451=CARTESIAN_POINT('Ctrl Pts',(3.21131386544667,1.31890422107427,4.73984673000161));
#63452=CARTESIAN_POINT('Ctrl Pts',(0.65013394439898,3.41018634994864,4.89784162100166));
#63453=CARTESIAN_POINT('Ctrl Pts',(-2.50081988404187,2.40789223066154,5.05583651200171));
#63454=CARTESIAN_POINT('Ctrl Pts',(-3.38313610732142,-0.77873947263813,
5.21383140300178));
#63455=CARTESIAN_POINT('Ctrl Pts',(-1.19641491396169,-3.25893179440594,
5.37182629400181));
#63456=CARTESIAN_POINT('Ctrl Pts',(2.07564308534076,-2.78275957804407,5.52982118500188));
#63457=CARTESIAN_POINT('Ctrl Pts',(3.46476581676266,0.217813961707557,5.68781607600192));
#63458=CARTESIAN_POINT('Ctrl Pts',(1.71080012542156,3.02079592455092,5.84581096700199));
#63459=CARTESIAN_POINT('Ctrl Pts',(-1.59513079308199,3.08344009831299,6.00380585800203));
#63460=CARTESIAN_POINT('Ctrl Pts',(-3.45402679099304,0.348918348651528,
6.1618007490021));
#63461=CARTESIAN_POINT('Ctrl Pts',(-2.17957635430163,-2.7021273106005,6.31979564000214));
#63462=CARTESIAN_POINT('Ctrl Pts',(1.07209319849625,-3.30191781555228,6.4777905310022));
#63463=CARTESIAN_POINT('Ctrl Pts',(3.35120532648497,-0.906348689336672,
6.63578542200224));
#63464=CARTESIAN_POINT('Ctrl Pts',(2.59024628631004,2.31142148107623,6.79378031300231));
#63465=CARTESIAN_POINT('Ctrl Pts',(-0.520474193792445,3.4323682349829,6.95177520400236));
#63466=CARTESIAN_POINT('Ctrl Pts',(-3.15904258646038,1.43961627660056,7.10977009500241));
#63467=CARTESIAN_POINT('Ctrl Pts',(-2.93186168880579,-1.85909443671817,
7.26776498600247));
#63468=CARTESIAN_POINT('Ctrl Pts',(-0.0450203642769841,-3.47131362076721,
7.42575987700253));
#63469=CARTESIAN_POINT('Ctrl Pts',(2.8826615230001,-1.93450449230244,7.58375476800256));
#63470=CARTESIAN_POINT('Ctrl Pts',(3.19531528460895,1.35720496568057,7.74174965900264));
#63471=CARTESIAN_POINT('Ctrl Pts',(0.609314704401862,3.41771571051825,7.89974455000267));
#63472=CARTESIAN_POINT('Ctrl Pts',(-2.52943030198254,2.37781989106326,8.05773944100274));
#63473=CARTESIAN_POINT('Ctrl Pts',(-3.37358354695964,-0.819133162926983,
8.21573433200278));
#63474=CARTESIAN_POINT('Ctrl Pts',(-1.15736505241679,-3.27300339479932,
8.37372922300284));
#63475=CARTESIAN_POINT('Ctrl Pts',(2.10876587186757,-2.75774393020277,8.53172411400289));
#63476=CARTESIAN_POINT('Ctrl Pts',(3.46191394284634,0.259223724318805,8.68971900500295));
#63477=CARTESIAN_POINT('Ctrl Pts',(1.67456068997757,3.04103462369395,8.847713896003));
#63478=CARTESIAN_POINT('Ctrl Pts',(-1.63188291307296,3.06414804553306,9.00570878700305));
#63479=CARTESIAN_POINT('Ctrl Pts',(-3.45795163290035,0.307596475021262,
9.16370367800311));
#63480=CARTESIAN_POINT('Ctrl Pts',(-2.14711346820945,-2.72799355599627,
9.32169856900316));
#63481=CARTESIAN_POINT('Ctrl Pts',(1.11149486081386,-3.28886367326282,9.47969346000322));
#63482=CARTESIAN_POINT('Ctrl Pts',(3.36180225010744,-0.866216322921951,
9.63768835100326));
#63483=CARTESIAN_POINT('Ctrl Pts',(2.56242539210976,2.34222569296695,9.79568324200333));
#63484=CARTESIAN_POINT('Ctrl Pts',(-0.561474971970195,3.42590001937795,
9.95367813300337));
#63485=CARTESIAN_POINT('Ctrl Pts',(-3.17602908369125,1.40174332403378,10.1116730240034));
#63486=CARTESIAN_POINT('Ctrl Pts',(-2.90942447610763,-1.8940153918983,10.2696679150035));
#63487=CARTESIAN_POINT('Ctrl Pts',(-0.0035135282481055,-3.47160377088719,
10.4276628060035));
#63488=CARTESIAN_POINT('Ctrl Pts',(2.90558474324488,-1.89990062549661,10.5856576970036));
#63489=CARTESIAN_POINT('Ctrl Pts',(3.17885991705762,1.39531169085301,10.7436525880036));
#63490=CARTESIAN_POINT('Ctrl Pts',(0.568408359757113,3.4247564911184,10.9016474790037));
#63491=CARTESIAN_POINT('Ctrl Pts',(-2.55767912491219,2.34740762992373,11.0596423700038));
#63492=CARTESIAN_POINT('Ctrl Pts',(-3.36354871550911,-0.859409753944302,
11.2176372610038));
#63493=CARTESIAN_POINT('Ctrl Pts',(-1.11814973965565,-3.2866071025492,11.3756321520039));
#63494=CARTESIAN_POINT('Ctrl Pts',(2.14158719959911,-2.73233404879208,11.5336270430039));
#63495=CARTESIAN_POINT('Ctrl Pts',(3.45856717040372,0.300596429689395,11.691621934004));
#63496=CARTESIAN_POINT('Ctrl Pts',(1.63808186784707,3.0608385911199,11.849616825004));
#63497=CARTESIAN_POINT('Ctrl Pts',(-1.66840174770112,3.04441795752144,12.0076117160041));
#63498=CARTESIAN_POINT('Ctrl Pts',(-3.46138214162631,0.266230628060431,
12.1656066070041));
#63499=CARTESIAN_POINT('Ctrl Pts',(-2.11434364366697,-2.75346981912873,
12.3236014980042));
#63500=CARTESIAN_POINT('Ctrl Pts',(1.15073763387882,-3.27533937411076,12.4815963890042));
#63501=CARTESIAN_POINT('Ctrl Pts',(3.37191857800943,-0.825960120600417,
12.6395912800043));
#63502=CARTESIAN_POINT('Ctrl Pts',(2.53423820298509,2.37269506052457,12.7975861710043));
#63503=CARTESIAN_POINT('Ctrl Pts',(-0.602395516750883,3.41894207513388,
12.9555810620044));
#63504=CARTESIAN_POINT('Ctrl Pts',(-3.19256148951789,1.3636699443205,13.1135759530045));
#63505=CARTESIAN_POINT('Ctrl Pts',(-2.8865714642773,-1.928665510007,13.2715708440045));
#63506=CARTESIAN_POINT('Ctrl Pts',(0.0379940355281645,-3.4713977862162,
13.4295657350046));
#63507=CARTESIAN_POINT('Ctrl Pts',(2.92809216447323,-1.8650248739301,13.5875606260046));
#63508=CARTESIAN_POINT('Ctrl Pts',(3.16195093823948,1.43321840602296,13.7455555170047));
#63509=CARTESIAN_POINT('Ctrl Pts',(0.527419185700519,3.43130872276077,13.9035504080047));
#63510=CARTESIAN_POINT('Ctrl Pts',(-2.58555931004217,2.31665781251357,14.0615452990048));
#63511=CARTESIAN_POINT('Ctrl Pts',(-3.35303878783672,-0.89955970052277,
14.2195401900048));
#63512=CARTESIAN_POINT('Ctrl Pts',(-1.07876361424012,-3.29974820917995,
14.3775350810049));
#63513=CARTESIAN_POINT('Ctrl Pts',(2.1740814221413,-2.70651974072904,14.5355299720049));
#63514=CARTESIAN_POINT('Ctrl Pts',(3.45476601337439,0.341899748256715,14.693524863005));
#63515=CARTESIAN_POINT('Ctrl Pts',(1.60129238166824,3.08025546489199,14.851519754005));
#63516=CARTESIAN_POINT('Ctrl Pts',(-1.70453592633028,3.02415622428451,15.0095146450051));
#63517=CARTESIAN_POINT('Ctrl Pts',(-3.46459709897726,0.225010999375169,
15.1675095360052));
#63518=CARTESIAN_POINT('Ctrl Pts',(-2.08073764888123,-2.77890487901232,
15.3255044270052));
#63519=CARTESIAN_POINT('Ctrl Pts',(1.18879279521126,-3.26067050402438,15.4834993180053));
#63520=CARTESIAN_POINT('Ctrl Pts',(3.38353434581409,-0.786904778499691,
15.6414942090053));
#63521=CARTESIAN_POINT('Ctrl Pts',(2.50166621690838,2.40558061866225,15.7994891000054));
#63522=CARTESIAN_POINT('Ctrl Pts',(0.411559545231536,3.07143639360967,15.9048190273387));
#63523=CARTESIAN_POINT('Ctrl Pts',(-0.545102916879006,2.891059807408,15.9574839910054));
#63524=CARTESIAN_POINT('Ctrl Pts',(-2.94111188951679,-0.00259486169482749,
14.1778238829104));
#63525=CARTESIAN_POINT('Ctrl Pts',(-2.94335307565858,-0.259762554464039,
14.1917293186085));
#63526=CARTESIAN_POINT('Ctrl Pts',(-2.91238767988341,-0.516399492336486,
14.2056347543067));
#63527=CARTESIAN_POINT('Ctrl Pts',(-2.84607967927153,-0.763554866459577,
14.2195401900048));
#63528=CARTESIAN_POINT('Ctrl Pts',(-2.59494706330453,-1.69962253674182,
14.2722051536715));
#63529=CARTESIAN_POINT('Ctrl Pts',(-1.83685533877235,-2.49968537296086,
14.3248701173382));
#63530=CARTESIAN_POINT('Ctrl Pts',(-0.915668637109368,-2.80084537966192,
14.3775350810049));
#63531=CARTESIAN_POINT('Ctrl Pts',(0.00551806455364026,-3.10200538636298,
14.4302000446716));
#63532=CARTESIAN_POINT('Ctrl Pts',(1.0897997433475,-2.90426256354601,14.4828650083382));
#63533=CARTESIAN_POINT('Ctrl Pts',(1.84538801461659,-2.29732123730656,14.5355299720049));
#63534=CARTESIAN_POINT('Ctrl Pts',(2.60097628588567,-1.6903799110671,14.5881949356716));
#63535=CARTESIAN_POINT('Ctrl Pts',(3.02787114963004,-0.674240081405173,
14.6408598993383));
#63536=CARTESIAN_POINT('Ctrl Pts',(2.93240630955118,0.29022245286501,14.693524863005));
#63537=CARTESIAN_POINT('Ctrl Pts',(2.83694146947232,1.25468498713517,14.7461898266717));
#63538=CARTESIAN_POINT('Ctrl Pts',(2.21911692557029,2.16747022601356,14.7988547903384));
#63539=CARTESIAN_POINT('Ctrl Pts',(1.35923326895286,2.61451297201819,14.851519754005));
#63540=CARTESIAN_POINT('Ctrl Pts',(0.499349612335403,3.06155571802283,14.9041847176717));
#63541=CARTESIAN_POINT('Ctrl Pts',(-0.602593156997484,3.04285597115367,
14.9568496813384));
#63542=CARTESIAN_POINT('Ctrl Pts',(-1.4469080704384,2.56698189356751,15.0095146450051));
#63543=CARTESIAN_POINT('Ctrl Pts',(-1.70601080500511,2.42094600950443,15.0256764300034));
#63544=CARTESIAN_POINT('Ctrl Pts',(-1.94085146734146,2.2318557880317,15.0418382150017));
#63545=CARTESIAN_POINT('Ctrl Pts',(-2.14373220034761,2.01193738948431,15.058));
#63546=CARTESIAN_POINT('Ctrl Pts',(-1.37994859234592,-1.93347131995891,
-1.83880688453542E-16));
#63547=CARTESIAN_POINT('Ctrl Pts',(-1.43831895271373,-1.90176082500493,
-1.96503831907269E-16));
#63548=CARTESIAN_POINT('Ctrl Pts',(-1.49514575458196,-1.86752259046863,
-3.60259795903682E-17));
#63549=CARTESIAN_POINT('Ctrl Pts',(-1.55024291463987,-1.83079524515745,
-1.11022302462516E-16));
#63550=CARTESIAN_POINT('Ctrl Pts',(-1.61820139003649,-1.78549464545158,
-1.89647209120044E-16));
#63551=CARTESIAN_POINT('Ctrl Pts',(-1.68352982136479,-1.73640902813589,
4.37133882625492E-17));
#63552=CARTESIAN_POINT('Ctrl Pts',(-1.74614398662112,-1.68389593204229,
2.08166817117217E-17));
#63553=CARTESIAN_POINT('Ctrl Pts',(-1.78291149355231,-1.65305984859862,
7.3715640875763E-18));
#63554=CARTESIAN_POINT('Ctrl Pts',(-1.81874277362574,-1.62104095184393,
-1.13501056944751E-16));
#63555=CARTESIAN_POINT('Ctrl Pts',(-1.85361742493061,-1.58790418430478,
-1.38777878078145E-16));
#63556=CARTESIAN_POINT('Ctrl Pts',(-1.86599100473682,-1.57614720832583,
-1.47746133009421E-16));
#63557=CARTESIAN_POINT('Ctrl Pts',(-1.87824533378606,-1.56424827137885,
6.18933070998169E-17));
#63558=CARTESIAN_POINT('Ctrl Pts',(-1.89037564784625,-1.55221386701801,
6.93889390390723E-18));
#63559=CARTESIAN_POINT('Ctrl Pts',(-1.9520612058093,-1.49101603289205,-2.72517484859507E-16));
#63560=CARTESIAN_POINT('Ctrl Pts',(-2.01038866542646,-1.42647262579372,
-5.93465220813464E-16));
#63561=CARTESIAN_POINT('Ctrl Pts',(-2.06526482907838,-1.35900295762991,
-3.95516952522712E-16));
#63562=CARTESIAN_POINT('Ctrl Pts',(-2.11328147227381,-1.29996699798658,
-2.22312217768304E-16));
#63563=CARTESIAN_POINT('Ctrl Pts',(-2.15865566139155,-1.2386893890933,-3.33360010116584E-16));
#63564=CARTESIAN_POINT('Ctrl Pts',(-2.20130818996771,-1.17541961668097,
-3.46944695195361E-16));
#63565=CARTESIAN_POINT('Ctrl Pts',(-2.22006840714514,-1.1475911452903,-3.52919760469855E-16));
#63566=CARTESIAN_POINT('Ctrl Pts',(-2.23830186692143,-1.11937693173939,
-3.24730293914024E-16));
#63567=CARTESIAN_POINT('Ctrl Pts',(-2.25600064404541,-1.09079672684346,
-3.05311331771918E-16));
#63568=CARTESIAN_POINT('Ctrl Pts',(-2.26668277274188,-1.07354709288677,
-2.93590982320615E-16));
#63569=CARTESIAN_POINT('Ctrl Pts',(-2.27717011522814,-1.05616412126237,
7.72460434588031E-17));
#63570=CARTESIAN_POINT('Ctrl Pts',(-2.28746078556243,-1.03865201740679,
1.38777878078145E-16));
#63571=CARTESIAN_POINT('Ctrl Pts',(-2.2952947631346,-1.02532057986291,1.85620211640871E-16));
#63572=CARTESIAN_POINT('Ctrl Pts',(-2.30301001735291,-1.01192234024488,
-2.74638834286083E-16));
#63573=CARTESIAN_POINT('Ctrl Pts',(-2.31060459934883,-0.99846213025753,
-2.77555756156289E-16));
#63574=CARTESIAN_POINT('Ctrl Pts',(-2.35418081118604,-0.921230103254969,
-2.94292477860916E-16));
#63575=CARTESIAN_POINT('Ctrl Pts',(-2.39380271969424,-0.841933889485626,
-3.78845217127159E-17));
#63576=CARTESIAN_POINT('Ctrl Pts',(-2.42937389319446,-0.760969916140703,
-6.93889390390723E-17));
#63577=CARTESIAN_POINT('Ctrl Pts',(-2.46720610926394,-0.674859556767564,
-1.02895900045749E-16));
#63578=CARTESIAN_POINT('Ctrl Pts',(-2.5004573035107,-0.586862180324133,
-9.42383278312778E-17));
#63579=CARTESIAN_POINT('Ctrl Pts',(-2.52897137574918,-0.497406668002497,
0.));
#63580=CARTESIAN_POINT('Ctrl Pts',(-2.55035692992803,-0.430315033761271,
7.06787458734584E-17));
#63581=CARTESIAN_POINT('Ctrl Pts',(-2.56907707912655,-0.362402071614612,
2.24154037051898E-16));
#63582=CARTESIAN_POINT('Ctrl Pts',(-2.58504714386116,-0.293835873442853,
2.77555756156289E-16));
#63583=CARTESIAN_POINT('Ctrl Pts',(-2.59702469241211,-0.242411224814034,
3.17607045484582E-16));
#63584=CARTESIAN_POINT('Ctrl Pts',(-2.60745499960513,-0.1906188874626,1.72939271916983E-16));
#63585=CARTESIAN_POINT('Ctrl Pts',(-2.61629539664834,-0.138527206391925,
1.38777878078145E-16));
#63586=CARTESIAN_POINT('Ctrl Pts',(-2.61869711284596,-0.124375191094725,
1.29497076264031E-16));
#63587=CARTESIAN_POINT('Ctrl Pts',(-2.62098183196127,-0.110198515695441,
1.70346493820844E-17));
#63588=CARTESIAN_POINT('Ctrl Pts',(-2.62314735205575,-0.0960068887486099,
2.77555756156289E-17));
#63589=CARTESIAN_POINT('Ctrl Pts',(-2.63712677206149,-0.00439346333649258,
9.69640447732094E-17));
#63590=CARTESIAN_POINT('Ctrl Pts',(-2.64610759043344,0.0876011416361361,
-2.12521409618605E-16));
#63591=CARTESIAN_POINT('Ctrl Pts',(-2.64996359474771,0.179577964648124,
-5.55111512312578E-17));
#63592=CARTESIAN_POINT('Ctrl Pts',(-2.65210628483955,0.230687302523444,
3.17357233945851E-17));
#63593=CARTESIAN_POINT('Ctrl Pts',(-2.65266584064783,0.281791760322423,
2.25858622101648E-16));
#63594=CARTESIAN_POINT('Ctrl Pts',(-2.65161463128253,0.332826444242184,
1.94289029309402E-16));
#63595=CARTESIAN_POINT('Ctrl Pts',(-2.64978728963931,0.421541220055518,
1.40408657934648E-16));
#63596=CARTESIAN_POINT('Ctrl Pts',(-2.6430958113368,0.510044886368098,1.72520161624302E-16));
#63597=CARTESIAN_POINT('Ctrl Pts',(-2.63178393076928,0.598076371345786,
1.66533453693773E-16));
#63598=CARTESIAN_POINT('Ctrl Pts',(-2.62024798910265,0.687851547937211,
1.60428163503557E-16));
#63599=CARTESIAN_POINT('Ctrl Pts',(-2.60390669120625,0.777136386959749,
-1.34425914858345E-16));
#63600=CARTESIAN_POINT('Ctrl Pts',(-2.58296460883121,0.865656938831555,
-1.11022302462516E-16));
#63601=CARTESIAN_POINT('Ctrl Pts',(-2.57869408333521,0.883708117645516,
-1.06249819877211E-16));
#63602=CARTESIAN_POINT('Ctrl Pts',(-2.57423206760738,0.901727502426255,
-4.70036822748448E-17));
#63603=CARTESIAN_POINT('Ctrl Pts',(-2.56958003501042,0.919712740461561,
-5.55111512312578E-17));
#63604=CARTESIAN_POINT('Ctrl Pts',(-2.56604635272843,0.933374320783267,
-6.19734215806574E-17));
#63605=CARTESIAN_POINT('Ctrl Pts',(-2.56240532303519,0.947007284078113,
8.26362614469453E-17));
#63606=CARTESIAN_POINT('Ctrl Pts',(-2.5586586911495,0.960608258314244,8.32667268468867E-17));
#63607=CARTESIAN_POINT('Ctrl Pts',(-2.53407091484386,1.04986648337083,8.74042409382574E-17));
#63608=CARTESIAN_POINT('Ctrl Pts',(-2.504930952964,1.13777933274063,7.81122475311754E-16));
#63609=CARTESIAN_POINT('Ctrl Pts',(-2.47152838793823,1.2240648243653,6.38378239159465E-16));
#63610=CARTESIAN_POINT('Ctrl Pts',(-2.43748524526305,1.31200505589874,4.92896525595146E-16));
#63611=CARTESIAN_POINT('Ctrl Pts',(-2.39901427145562,1.39825569878996,-4.49689980744232E-17));
#63612=CARTESIAN_POINT('Ctrl Pts',(-2.35636659634517,1.48252101187545,-5.55111512312578E-17));
#63613=CARTESIAN_POINT('Ctrl Pts',(-2.31336109209446,1.56749334086406,-6.61417567970626E-17));
#63614=CARTESIAN_POINT('Ctrl Pts',(-2.26610821171127,1.65044775809861,-5.44480906746773E-17));
#63615=CARTESIAN_POINT('Ctrl Pts',(-2.21481327415801,1.731071203515,-5.55111512312578E-17));
#63616=CARTESIAN_POINT('Ctrl Pts',(-2.18401751630642,1.77947481253834,-5.61493770883036E-17));
#63617=CARTESIAN_POINT('Ctrl Pts',(-2.15176385823466,1.82703799978858,3.67516605336294E-16));
#63618=CARTESIAN_POINT('Ctrl Pts',(-2.11808850376184,1.87368930169054,3.88578058618805E-16));
#63619=CARTESIAN_POINT('Ctrl Pts',(-2.1089145366433,1.88639822536441,3.94315699184355E-16));
#63620=CARTESIAN_POINT('Ctrl Pts',(-2.09963412322397,1.89904053530927,1.84615714870052E-16));
#63621=CARTESIAN_POINT('Ctrl Pts',(-2.09025911328956,1.91160012317952,1.66533453693773E-16));
#63622=CARTESIAN_POINT('Ctrl Pts',(-2.03145402967869,1.99038058527982,5.31118266465956E-17));
#63623=CARTESIAN_POINT('Ctrl Pts',(-1.96883756375661,2.06603912302101,4.62847422951145E-16));
#63624=CARTESIAN_POINT('Ctrl Pts',(-1.90268196527442,2.13826743811961,3.33066907387547E-16));
#63625=CARTESIAN_POINT('Ctrl Pts',(-1.83635976195865,2.21067765145044,2.0295955537029E-16));
#63626=CARTESIAN_POINT('Ctrl Pts',(-1.76648017672323,2.2796412428746,3.28001727774597E-18));
#63627=CARTESIAN_POINT('Ctrl Pts',(-1.6932675195623,2.34483179093341,0.));
#63628=CARTESIAN_POINT('Ctrl Pts',(-1.62146081066126,2.40877044429043,-3.21702906282713E-18));
#63629=CARTESIAN_POINT('Ctrl Pts',(-1.54644728359632,2.46908034426641,-8.3280583097932E-18));
#63630=CARTESIAN_POINT('Ctrl Pts',(-1.46839770082455,2.52542611967769,-5.55111512312578E-17));
#63631=CARTESIAN_POINT('Ctrl Pts',(-1.41023968234018,2.56741172077267,-9.06692532072844E-17));
#63632=CARTESIAN_POINT('Ctrl Pts',(-1.35039506896231,2.60719581243537,-1.11866688105539E-17));
#63633=CARTESIAN_POINT('Ctrl Pts',(-1.28892185405323,2.64462557919718,0.));
#63634=CARTESIAN_POINT('Origin',(0.,0.,0.));
#63635=CARTESIAN_POINT('Origin',(-1.44337567297407,-2.5,-6.));
#63636=CARTESIAN_POINT('',(-1.44337567297407,-2.5,-6.));
#63637=CARTESIAN_POINT('',(1.44337567297406,-2.5,-6.));
#63638=CARTESIAN_POINT('',(-0.721687836487033,-2.5,-6.));
#63639=CARTESIAN_POINT('',(-1.44337567297407,-2.5,-3.));
#63640=CARTESIAN_POINT('',(-1.44337567297407,-2.5,-6.));
#63641=CARTESIAN_POINT('',(1.44337567297406,-2.5,-3.));
#63642=CARTESIAN_POINT('',(-1.44337567297407,-2.5,-3.));
#63643=CARTESIAN_POINT('',(1.44337567297406,-2.5,-6.));
#63644=CARTESIAN_POINT('Origin',(-2.88675134594813,3.53525079574969E-16,
-6.));
#63645=CARTESIAN_POINT('',(-2.88675134594813,3.53525079574969E-16,-6.));
#63646=CARTESIAN_POINT('',(-2.52590742770461,-0.625,-6.));
#63647=CARTESIAN_POINT('',(-2.88675134594813,5.55111512312578E-16,-3.));
#63648=CARTESIAN_POINT('',(-2.88675134594813,3.53525079574969E-16,-6.));
#63649=CARTESIAN_POINT('',(-2.88675134594813,3.53525079574969E-16,-3.));
#63650=CARTESIAN_POINT('Origin',(-1.44337567297406,2.5,-6.));
#63651=CARTESIAN_POINT('',(-1.44337567297406,2.5,-6.));
#63652=CARTESIAN_POINT('',(-1.80421959121758,1.875,-6.));
#63653=CARTESIAN_POINT('',(-1.44337567297406,2.5,-3.));
#63654=CARTESIAN_POINT('',(-1.44337567297406,2.5,-6.));
#63655=CARTESIAN_POINT('',(-1.44337567297406,2.5,-3.));
#63656=CARTESIAN_POINT('Origin',(1.44337567297406,2.5,-6.));
#63657=CARTESIAN_POINT('',(1.44337567297406,2.5,-6.));
#63658=CARTESIAN_POINT('',(0.721687836487033,2.5,-6.));
#63659=CARTESIAN_POINT('',(1.44337567297406,2.5,-3.));
#63660=CARTESIAN_POINT('',(1.44337567297406,2.5,-6.));
#63661=CARTESIAN_POINT('',(1.44337567297406,2.5,-3.));
#63662=CARTESIAN_POINT('Origin',(2.88675134594813,0.,-6.));
#63663=CARTESIAN_POINT('',(2.88675134594813,0.,-6.));
#63664=CARTESIAN_POINT('',(2.52590742770461,0.625,-6.));
#63665=CARTESIAN_POINT('',(2.88675134594813,0.,-3.));
#63666=CARTESIAN_POINT('',(2.88675134594813,0.,-6.));
#63667=CARTESIAN_POINT('',(2.88675134594813,0.,-3.));
#63668=CARTESIAN_POINT('Origin',(1.44337567297406,-2.5,-6.));
#63669=CARTESIAN_POINT('',(1.80421959121758,-1.875,-6.));
#63670=CARTESIAN_POINT('',(1.44337567297406,-2.5,-3.));
#63671=CARTESIAN_POINT('Origin',(0.,0.,-3.));
#63672=CARTESIAN_POINT('Origin',(0.,0.,0.));
#63673=CARTESIAN_POINT('',(-5.,-6.12323399573677E-16,0.));
#63674=CARTESIAN_POINT('Origin',(0.,0.,0.));
#63675=CARTESIAN_POINT('Origin',(0.,0.,-6.));
#63676=CARTESIAN_POINT('',(-5.,-6.12323399573677E-16,-6.));
#63677=CARTESIAN_POINT('',(-5.,-6.12323399573677E-16,-6.));
#63678=CARTESIAN_POINT('Origin',(0.,0.,-6.));
#63679=CARTESIAN_POINT('Origin',(0.,0.,-6.));
#63680=CARTESIAN_POINT('Origin',(0.,0.,16.));
#63733=UNCERTAINTY_MEASURE_WITH_UNIT(LENGTH_MEASURE(0.01),#63756,
'DISTANCE_ACCURACY_VALUE',
'Maximum model space distance between geometric entities at asserted c
onnectivities');
#63735=UNCERTAINTY_MEASURE_WITH_UNIT(LENGTH_MEASURE(0.01),#63756,
'DISTANCE_ACCURACY_VALUE',
'Maximum model space distance between geometric entities at asserted c
onnectivities');
#63753=(
GEOMETRIC_REPRESENTATION_CONTEXT(3)
GLOBAL_UNCERTAINTY_ASSIGNED_CONTEXT((#63733))
GLOBAL_UNIT_ASSIGNED_CONTEXT((#63756,#63758,#63759))
REPRESENTATION_CONTEXT('','3D')
);
#63755=(
GEOMETRIC_REPRESENTATION_CONTEXT(3)
GLOBAL_UNCERTAINTY_ASSIGNED_CONTEXT((#63735))
GLOBAL_UNIT_ASSIGNED_CONTEXT((#63756,#63758,#63759))
REPRESENTATION_CONTEXT('','3D')
);
#63756=(
LENGTH_UNIT()
NAMED_UNIT(*)
SI_UNIT(.MILLI.,.METRE.)
);
#63758=(
NAMED_UNIT(*)
PLANE_ANGLE_UNIT()
SI_UNIT($,.RADIAN.)
);
#63759=(
NAMED_UNIT(*)
SI_UNIT($,.STERADIAN.)
SOLID_ANGLE_UNIT()
);
#63777=SHAPE_DEFINITION_REPRESENTATION(#63836,#63875);
#63836=PRODUCT_DEFINITION_SHAPE('',$,#63895);
#63875=SHAPE_REPRESENTATION('',(#15434),#63753);
#63877=PRODUCT_DEFINITION_CONTEXT('part definition',#63936,'design');
#63895=PRODUCT_DEFINITION('Socket head cap screw M6x16',
'Socket head cap screw M6x16',#63914,#63877);
#63914=PRODUCT_DEFINITION_FORMATION('',$,#63955);
#63936=APPLICATION_CONTEXT(
'Core Data for Automotive Mechanical Design Process');
#63937=PRODUCT_CONTEXT('part definition',#63936,'mechanical');
#63955=PRODUCT('Socket head cap screw M6x16',
'Socket head cap screw M6x16',$,(#63937));
#63960=PRESENTATION_STYLE_ASSIGNMENT((#63967));
#63967=SURFACE_STYLE_USAGE(.BOTH.,#63974);
#63974=SURFACE_SIDE_STYLE('',(#63981));
#63981=SURFACE_STYLE_FILL_AREA(#63988);
#63988=FILL_AREA_STYLE('Dark gray',(#63995));
#63995=FILL_AREA_STYLE_COLOUR('Dark gray',#64002);
#64002=COLOUR_RGB('Dark gray',0.250980392156863,0.282352941176471,0.32156862745098);
ENDSEC;
END-ISO-10303-21;
